ISO-10303-21;
HEADER;
FILE_DESCRIPTION (('STEP AP214'),
    '1' );
FILE_NAME ('spur gear_iso_ISO - Spur gear 3M 20T 20PA 10FW ---S20A75H50L10.0S1.step',
    '2026-10-24T07:08:27',
    ( '' ),
    ( '' ),
    'SwSTEP 2.0',
    'SolidWorks 2026',
    '' );
FILE_SCHEMA (( 'AUTOMOTIVE_DESIGN' ));
ENDSEC;

DATA;
#2=VECTOR ( 'NONE', #14749, 1000.000000000000000 ) ;
#7=DIRECTION ( 'NONE',  ( 0.000000000000000000, 0.000000000000000000, 1.000000000000000000 ) ) ;
#10=DIRECTION ( 'NONE',  ( -1.000000000000000000, 0.000000000000000000, 0.000000000000000000 ) ) ;
#13=CARTESIAN_POINT ( 'NONE',  ( 0.000000000000000000, 0.000000000000000000, 0.000000000000000000 ) ) ;
#21=CIRCLE ( 'NONE', #6696, 12.00000000001200462 ) ;
#22=CARTESIAN_POINT ( 'NONE',  ( 10.00000000000000000, 14.27431201565567065, -29.75305054077457356 ) ) ;
#24=VERTEX_POINT ( 'NONE', #17163 ) ;
#25=CARTESIAN_POINT ( 'NONE',  ( 10.00000000000000000, -5.086963483077402870, 27.72801475327280585 ) ) ;
#26=DIRECTION ( 'NONE',  ( 0.000000000000000000, 0.3090169943749410120, 0.9510565162951556406 ) ) ;
#31=DIRECTION ( 'NONE',  ( 0.000000000000000000, -1.000000000000000000, 0.000000000000000000 ) ) ;
#32=CARTESIAN_POINT ( 'NONE',  ( 10.00000000000000000, 0.000000000000000000, 0.000000000000000000 ) ) ;
#34=VERTEX_POINT ( 'NONE', #6862 ) ;
#38=VERTEX_POINT ( 'NONE', #8302 ) ;
#46=ADVANCED_FACE ( 'NONE', ( #14203 ), #12781, .T. ) ;
#53=EDGE_CURVE ( 'NONE', #16495, #2470, #11654, .T. ) ;
#61=ORIENTED_EDGE ( 'NONE', *, *, #6083, .F. ) ;
#73=DIRECTION ( 'NONE',  ( 1.000000000000000000, 0.000000000000000000, 0.000000000000000000 ) ) ;
#75=ORIENTED_EDGE ( 'NONE', *, *, #4136, .T. ) ;
#82=ORIENTED_EDGE ( 'NONE', *, *, #16007, .F. ) ;
#83=ORIENTED_EDGE ( 'NONE', *, *, #2311, .T. ) ;
#85=( LENGTH_UNIT ( ) NAMED_UNIT ( * ) SI_UNIT ( .MILLI., .METRE. ) );
#86=ORIENTED_EDGE ( 'NONE', *, *, #2865, .F. ) ;
#100=DIRECTION ( 'NONE',  ( -1.000000000000000000, 0.000000000000000000, 0.000000000000000000 ) ) ;
#102=CIRCLE ( 'NONE', #1309, 33.00000000003299760 ) ;
#103=DIRECTION ( 'NONE',  ( -1.000000000000000000, -0.000000000000000000, 0.000000000000000000 ) ) ;
#107=CARTESIAN_POINT ( 'NONE',  ( 50.00005079999999680, 0.000000000000000000, 0.000000000000000000 ) ) ;
#110=CYLINDRICAL_SURFACE ( 'NONE', #16518, 26.24900000002624978 ) ;
#128=ORIENTED_EDGE ( 'NONE', *, *, #5149, .F. ) ;
#133=FACE_OUTER_BOUND ( 'NONE', #8514, .T. ) ;
#140=ADVANCED_FACE ( 'NONE', ( #1619 ), #11545, .F. ) ;
#144=DIRECTION ( 'NONE',  ( 0.000000000000000000, -0.5877852522924624790, -0.8090169943749551118 ) ) ;
#147=CARTESIAN_POINT ( 'NONE',  ( 10.00000000000000000, -26.20671763660629594, 1.489278925039428936 ) ) ;
#153=CARTESIAN_POINT ( 'NONE',  ( 0.000000000000000000, -29.75305054077482581, 14.27431201565513952 ) ) ;
#172=DIRECTION ( 'NONE',  ( -1.000000000000000000, 0.000000000000000000, 0.000000000000000000 ) ) ;
#178=CARTESIAN_POINT ( 'NONE',  ( 0.000000000000000000, 6.799999999999999822, 1.500000000000000000 ) ) ;
#181=ORIENTED_EDGE ( 'NONE', *, *, #5658, .T. ) ;
#184=CARTESIAN_POINT ( 'NONE',  ( 10.00000000000000000, -14.19907017806852245, -22.07705612348854984 ) ) ;
#190=AXIS2_PLACEMENT_3D ( 'NONE', #10322, #1927, #7639 ) ;
#195=VERTEX_POINT ( 'NONE', #22 ) ;
#196=CARTESIAN_POINT ( 'NONE',  ( 10.00000000000000178, 6.799999999999999822, 1.500000000000000000 ) ) ;
#198=EDGE_CURVE ( 'NONE', #10779, #13712, #7678, .T. ) ;
#203=CARTESIAN_POINT ( 'NONE',  ( 10.00000000000000000, 0.000000000000000000, 0.000000000000000000 ) ) ;
#205=VERTEX_POINT ( 'NONE', #10192 ) ;
#207=DIRECTION ( 'NONE',  ( 0.000000000000000000, 0.000000000000000000, 1.000000000000000000 ) ) ;
#214=CIRCLE ( 'NONE', #13847, 12.00000000001200462 ) ;
#223=AXIS2_PLACEMENT_3D ( 'NONE', #7888, #16549, #14847 ) ;
#228=ADVANCED_FACE ( 'NONE', ( #13154 ), #110, .T. ) ;
#231=DIRECTION ( 'NONE',  ( -1.000000000000000000, 0.000000000000000000, -0.000000000000000000 ) ) ;
#234=ORIENTED_EDGE ( 'NONE', *, *, #4136, .F. ) ;
#236=CARTESIAN_POINT ( 'NONE',  ( 10.00000000000000000, 0.000000000000000000, 0.000000000000000000 ) ) ;
#253=ORIENTED_EDGE ( 'NONE', *, *, #16333, .F. ) ;
#259=ORIENTED_EDGE ( 'NONE', *, *, #7474, .F. ) ;
#262=VERTEX_POINT ( 'NONE', #3626 ) ;
#264=AXIS2_PLACEMENT_3D ( 'NONE', #7455, #9080, #11756 ) ;
#270=EDGE_CURVE ( 'NONE', #10074, #2470, #10746, .T. ) ;
#272=EDGE_CURVE ( 'NONE', #1366, #4272, #1923, .T. ) ;
#279=CARTESIAN_POINT ( 'NONE',  ( 10.00000000000000000, 22.07705612348859958, -14.19907017806844252 ) ) ;
#285=CARTESIAN_POINT ( 'NONE',  ( 0.000000000000000000, -22.76987570971509811, -23.88582760061506249 ) ) ;
#289=CARTESIAN_POINT ( 'NONE',  ( 10.00000000000000000, 25.38428207620322752, 6.681932690257054830 ) ) ;
#292=DIRECTION ( 'NONE',  ( 0.000000000000000000, -0.3090169943749348502, -0.9510565162951576390 ) ) ;
#307=CIRCLE ( 'NONE', #11570, 12.00000000001200640 ) ;
#309=CYLINDRICAL_SURFACE ( 'NONE', #6869, 26.24900000002624978 ) ;
#320=VECTOR ( 'NONE', #10301, 1000.000000000000000 ) ;
#322=CARTESIAN_POINT ( 'NONE',  ( 10.00000000000000000, 3.730438010304726770, -27.94286728106388296 ) ) ;
#332=CARTESIAN_POINT ( 'NONE',  ( 10.00000000000000000, 0.000000000000000000, 0.000000000000000000 ) ) ;
#334=EDGE_LOOP ( 'NONE', ( #9936, #9386, #7839, #1385 ) ) ;
#341=EDGE_CURVE ( 'NONE', #9120, #6839, #4855, .T. ) ;
#343=DIRECTION ( 'NONE',  ( 0.000000000000000000, 0.000000000000000000, -1.000000000000000000 ) ) ;
#344=DIRECTION ( 'NONE',  ( 0.000000000000000000, 0.000000000000000000, 1.000000000000000000 ) ) ;
#353=VERTEX_POINT ( 'NONE', #13434 ) ;
#364=VERTEX_POINT ( 'NONE', #13623 ) ;
#377=DIRECTION ( 'NONE',  ( 0.000000000000000000, 0.3090169943749479509, -0.9510565162951533091 ) ) ;
#378=DIRECTION ( 'NONE',  ( 1.000000000000000000, 0.000000000000000000, 0.000000000000000000 ) ) ;
#381=AXIS2_PLACEMENT_3D ( 'NONE', #3992, #9793, #15604 ) ;
#382=CARTESIAN_POINT ( 'NONE',  ( 10.00000000000000000, 32.46095361140700675, -5.940243314903877803 ) ) ;
#400=ORIENTED_EDGE ( 'NONE', *, *, #15230, .T. ) ;
#408=CARTESIAN_POINT ( 'NONE',  ( 10.00000000000000000, -27.94286728106395756, 3.730438010304225394 ) ) ;
#419=DIRECTION ( 'NONE',  ( -1.000000000000000000, 0.000000000000000000, -0.000000000000000000 ) ) ;
#437=ORIENTED_EDGE ( 'NONE', *, *, #12143, .T. ) ;
#439=DIRECTION ( 'NONE',  ( 0.000000000000000000, 0.000000000000000000, 1.000000000000000000 ) ) ;
#446=CARTESIAN_POINT ( 'NONE',  ( -10.00000000000000000, 0.000000000000000000, 0.000000000000000000 ) ) ;
#447=EDGE_CURVE ( 'NONE', #5630, #6042, #11910, .T. ) ;
#462=ORIENTED_EDGE ( 'NONE', *, *, #18236, .F. ) ;
#464=CYLINDRICAL_SURFACE ( 'NONE', #11147, 12.00000000001200817 ) ;
#477=DIRECTION ( 'NONE',  ( 0.000000000000000000, 0.000000000000000000, 1.000000000000000000 ) ) ;
#482=DIRECTION ( 'NONE',  ( 0.000000000000000000, 0.000000000000000000, 1.000000000000000000 ) ) ;
#498=ORIENTED_EDGE ( 'NONE', *, *, #10985, .T. ) ;
#510=AXIS2_PLACEMENT_3D ( 'NONE', #13465, #13552, #17930 ) ;
#514=VERTEX_POINT ( 'NONE', #12562 ) ;
#516=CARTESIAN_POINT ( 'NONE',  ( 10.00000000000000000, 0.000000000000000000, -1.500000000000000000 ) ) ;
#517=CARTESIAN_POINT ( 'NONE',  ( 10.00000000000000000, -27.72801475327285559, 5.086963483077107995 ) ) ;
#519=CARTESIAN_POINT ( 'NONE',  ( 50.00005079999999680, 6.799999999999999822, -1.500000000000000000 ) ) ;
#530=AXIS2_PLACEMENT_3D ( 'NONE', #4970, #11933, #16504 ) ;
#534=DIRECTION ( 'NONE',  ( 1.000000000000000000, -0.000000000000000000, -0.000000000000000000 ) ) ;
#539=DIRECTION ( 'NONE',  ( 1.000000000000000000, 0.000000000000000000, 0.000000000000000000 ) ) ;
#540=EDGE_LOOP ( 'NONE', ( #9099, #3031, #14375, #5789 ) ) ;
#545=AXIS2_PLACEMENT_3D ( 'NONE', #3110, #11499, #10065 ) ;
#561=FACE_OUTER_BOUND ( 'NONE', #18564, .T. ) ;
#566=CARTESIAN_POINT ( 'NONE',  ( 10.00000000000000000, 27.72801475327282361, 6.913036516934699449 ) ) ;
#573=CIRCLE ( 'NONE', #10906, 33.00000000003299760 ) ;
#585=CYLINDRICAL_SURFACE ( 'NONE', #13933, 33.00000000003299760 ) ;
#587=ORIENTED_EDGE ( 'NONE', *, *, #5226, .T. ) ;
#599=CIRCLE ( 'NONE', #2110, 33.00000000003299760 ) ;
#608=FACE_OUTER_BOUND ( 'NONE', #1873, .T. ) ;
#621=CIRCLE ( 'NONE', #2138, 33.00000000003299760 ) ;
#628=ORIENTED_EDGE ( 'NONE', *, *, #3896, .T. ) ;
#633=CARTESIAN_POINT ( 'NONE',  ( 10.00000000000000000, 27.72801475327282361, -5.086963483077305170 ) ) ;
#636=VECTOR ( 'NONE', #11597, 1000.000000000000000 ) ;
#637=DIRECTION ( 'NONE',  ( -1.000000000000000000, 0.000000000000000000, 0.000000000000000000 ) ) ;
#642=CARTESIAN_POINT ( 'NONE',  ( 10.00000000000000000, 0.000000000000000000, 0.000000000000000000 ) ) ;
#643=( NAMED_UNIT ( * ) PLANE_ANGLE_UNIT ( ) SI_UNIT ( $, .RADIAN. ) );
#646=LINE ( 'NONE', #15390, #12767 ) ;
#650=DIRECTION ( 'NONE',  ( -1.000000000000000000, -0.000000000000000000, -0.000000000000000000 ) ) ;
#651=CARTESIAN_POINT ( 'NONE',  ( 10.00000000000000000, -27.94286728106395756, 15.73043801031622912 ) ) ;
#659=DIRECTION ( 'NONE',  ( -1.000000000000000000, -0.000000000000000000, -0.000000000000000000 ) ) ;
#660=DIRECTION ( 'NONE',  ( -1.000000000000000000, 0.000000000000000000, -0.000000000000000000 ) ) ;
#662=ORIENTED_EDGE ( 'NONE', *, *, #2383, .T. ) ;
#667=CARTESIAN_POINT ( 'NONE',  ( 5.000000000000000000, 4.381479206522992165, 32.70783759231088084 ) ) ;
#681=EDGE_CURVE ( 'NONE', #6992, #16250, #13353, .T. ) ;
#684=VERTEX_POINT ( 'NONE', #16240 ) ;
#695=DIRECTION ( 'NONE',  ( 0.000000000000000000, 0.000000000000000000, 1.000000000000000000 ) ) ;
#702=CYLINDRICAL_SURFACE ( 'NONE', #5436, 26.24900000002624978 ) ;
#703=ORIENTED_EDGE ( 'NONE', *, *, #8448, .F. ) ;
#710=ORIENTED_EDGE ( 'NONE', *, *, #5586, .F. ) ;
#716=ORIENTED_EDGE ( 'NONE', *, *, #12750, .F. ) ;
#724=DIRECTION ( 'NONE',  ( -1.000000000000000000, 0.000000000000000000, 0.000000000000000000 ) ) ;
#725=EDGE_CURVE ( 'NONE', #9332, #10957, #11102, .T. ) ;
#726=VERTEX_POINT ( 'NONE', #2047 ) ;
#731=CYLINDRICAL_SURFACE ( 'NONE', #17532, 33.00000000003299760 ) ;
#744=EDGE_CURVE ( 'NONE', #4042, #7876, #15574, .T. ) ;
#748=ORIENTED_EDGE ( 'NONE', *, *, #17754, .T. ) ;
#751=CARTESIAN_POINT ( 'NONE',  ( 0.000000000000000000, 0.000000000000000000, 0.000000000000000000 ) ) ;
#754=EDGE_CURVE ( 'NONE', #8328, #17358, #3852, .T. ) ;
#758=DIRECTION ( 'NONE',  ( -1.000000000000000000, 0.000000000000000000, 0.000000000000000000 ) ) ;
#771=CARTESIAN_POINT ( 'NONE',  ( 10.00000000000000178, 4.769696007084728073, -1.500000000000000000 ) ) ;
#772=DIRECTION ( 'NONE',  ( -1.000000000000000000, 0.000000000000000000, 0.000000000000000000 ) ) ;
#774=DIRECTION ( 'NONE',  ( -1.000000000000000000, 0.000000000000000000, 0.000000000000000000 ) ) ;
#775=CIRCLE ( 'NONE', #16575, 33.00000000003299760 ) ;
#777=ORIENTED_EDGE ( 'NONE', *, *, #16572, .T. ) ;
#778=CARTESIAN_POINT ( 'NONE',  ( 10.00000000000000000, 0.000000000000000000, 0.000000000000000000 ) ) ;
#783=ORIENTED_EDGE ( 'NONE', *, *, #6803, .T. ) ;
#792=DIRECTION ( 'NONE',  ( 0.000000000000000000, 0.000000000000000000, 1.000000000000000000 ) ) ;
#793=DIRECTION ( 'NONE',  ( -1.000000000000000000, 0.000000000000000000, -0.000000000000000000 ) ) ;
#808=VERTEX_POINT ( 'NONE', #14043 ) ;
#816=AXIS2_PLACEMENT_3D ( 'NONE', #18020, #17933, #4886 ) ;
#817=CARTESIAN_POINT ( 'NONE',  ( 0.000000000000000000, 6.799999999999999822, 0.000000000000000000 ) ) ;
#821=DIRECTION ( 'NONE',  ( -1.000000000000000000, -0.000000000000000000, -0.000000000000000000 ) ) ;
#828=ORIENTED_EDGE ( 'NONE', *, *, #3325, .T. ) ;
#837=AXIS2_PLACEMENT_3D ( 'NONE', #16398, #9235, #12097 ) ;
#850=CIRCLE ( 'NONE', #13002, 12.00000000001200462 ) ;
#851=DIRECTION ( 'NONE',  ( -1.000000000000000000, 0.000000000000000000, 0.000000000000000000 ) ) ;
#852=DIRECTION ( 'NONE',  ( 0.000000000000000000, 0.000000000000000000, -1.000000000000000000 ) ) ;
#854=DIRECTION ( 'NONE',  ( 0.000000000000000000, 0.000000000000000000, 1.000000000000000000 ) ) ;
#861=ORIENTED_EDGE ( 'NONE', *, *, #11844, .T. ) ;
#864=AXIS2_PLACEMENT_3D ( 'NONE', #16750, #15599, #6828 ) ;
#868=EDGE_CURVE ( 'NONE', #8500, #11257, #8513, .T. ) ;
#873=VECTOR ( 'NONE', #3004, 1000.000000000000000 ) ;
#877=DIRECTION ( 'NONE',  ( 1.000000000000000000, 0.000000000000000000, 0.000000000000000000 ) ) ;
#887=DIRECTION ( 'NONE',  ( 1.000000000000000000, 0.000000000000000000, 0.000000000000000000 ) ) ;
#890=VERTEX_POINT ( 'NONE', #2425 ) ;
#901=FACE_OUTER_BOUND ( 'NONE', #11513, .T. ) ;
#914=CARTESIAN_POINT ( 'NONE',  ( 10.00000000000000000, 0.000000000000000000, 0.000000000000000000 ) ) ;
#921=DIRECTION ( 'NONE',  ( 0.000000000000000000, 0.000000000000000000, -1.000000000000000000 ) ) ;
#923=VERTEX_POINT ( 'NONE', #15566 ) ;
#925=ORIENTED_EDGE ( 'NONE', *, *, #7615, .T. ) ;
#928=CARTESIAN_POINT ( 'NONE',  ( 10.00000000000000000, -27.72801475327278453, -5.086963483077506787 ) ) ;
#937=CARTESIAN_POINT ( 'NONE',  ( -10.00000000000000000, 0.000000000000000000, 0.000000000000000000 ) ) ;
#941=VERTEX_POINT ( 'NONE', #5479 ) ;
#942=DIRECTION ( 'NONE',  ( -1.000000000000000000, 0.000000000000000000, 0.000000000000000000 ) ) ;
#944=VERTEX_POINT ( 'NONE', #4050 ) ;
#947=CARTESIAN_POINT ( 'NONE',  ( 0.000000000000000000, 5.940243314904670946, -32.46095361140686464 ) ) ;
#952=DIRECTION ( 'NONE',  ( -1.000000000000000000, 0.000000000000000000, 0.000000000000000000 ) ) ;
#954=ORIENTED_EDGE ( 'NONE', *, *, #16912, .F. ) ;
#958=EDGE_LOOP ( 'NONE', ( #6895, #6148, #2898, #7199 ) ) ;
#965=AXIS2_PLACEMENT_3D ( 'NONE', #3766, #2330, #12151 ) ;
#972=CARTESIAN_POINT ( 'NONE',  ( 10.00000000000000000, 1.489278925039520418, 26.20671763660628883 ) ) ;
#973=AXIS2_PLACEMENT_3D ( 'NONE', #2003, #13534, #482 ) ;
#976=EDGE_CURVE ( 'NONE', #6348, #14291, #9950, .T. ) ;
#977=ORIENTED_EDGE ( 'NONE', *, *, #6473, .T. ) ;
#978=ORIENTED_EDGE ( 'NONE', *, *, #14408, .T. ) ;
#984=CARTESIAN_POINT ( 'NONE',  ( 10.00000000000000000, 0.000000000000000000, 0.000000000000000000 ) ) ;
#1013=ORIENTED_EDGE ( 'NONE', *, *, #9491, .T. ) ;
#1019=EDGE_CURVE ( 'NONE', #13886, #4065, #8289, .T. ) ;
#1022=ORIENTED_EDGE ( 'NONE', *, *, #2377, .T. ) ;
#1032=DIRECTION ( 'NONE',  ( 1.000000000000000000, -0.000000000000000000, 0.000000000000000000 ) ) ;
#1036=ORIENTED_EDGE ( 'NONE', *, *, #3420, .F. ) ;
#1042=EDGE_CURVE ( 'NONE', #14980, #3488, #16030, .T. ) ;
#1045=DIRECTION ( 'NONE',  ( 0.000000000000000000, 0.000000000000000000, 1.000000000000000000 ) ) ;
#1057=CARTESIAN_POINT ( 'NONE',  ( 0.000000000000000000, 20.41355805489615705, 19.44239304137382973 ) ) ;
#1058=ORIENTED_EDGE ( 'NONE', *, *, #7053, .T. ) ;
#1063=DIRECTION ( 'NONE',  ( -1.000000000000000000, -0.000000000000000000, 0.000000000000000000 ) ) ;
#1064=AXIS2_PLACEMENT_3D ( 'NONE', #13787, #851, #4931 ) ;
#1072=CIRCLE ( 'NONE', #13240, 12.00000000001200462 ) ;
#1074=AXIS2_PLACEMENT_3D ( 'NONE', #18222, #3466, #9453 ) ;
#1076=CARTESIAN_POINT ( 'NONE',  ( 50.00005079999999680, 6.799999999999999822, 1.500000000000000000 ) ) ;
#1080=ADVANCED_FACE ( 'NONE', ( #15331 ), #7997, .T. ) ;
#1083=ORIENTED_EDGE ( 'NONE', *, *, #7405, .T. ) ;
#1091=VERTEX_POINT ( 'NONE', #771 ) ;
#1097=CYLINDRICAL_SURFACE ( 'NONE', #11726, 12.00000000001200462 ) ;
#1098=EDGE_CURVE ( 'NONE', #9858, #9496, #5683, .T. ) ;
#1104=EDGE_CURVE ( 'NONE', #5754, #8001, #16320, .T. ) ;
#1113=ORIENTED_EDGE ( 'NONE', *, *, #7721, .T. ) ;
#1118=CARTESIAN_POINT ( 'NONE',  ( 10.00000000000000000, 16.60877409751197575, -20.32630374611166957 ) ) ;
#1119=AXIS2_PLACEMENT_3D ( 'NONE', #4299, #11626, #1616 ) ;
#1128=EDGE_LOOP ( 'NONE', ( #12006, #3381, #1622, #7072 ) ) ;
#1134=CARTESIAN_POINT ( 'NONE',  ( 0.000000000000000000, 15.68049343256038064, -29.03656532225546627 ) ) ;
#1135=ORIENTED_EDGE ( 'NONE', *, *, #868, .T. ) ;
#1147=CIRCLE ( 'NONE', #223, 12.00000000001200107 ) ;
#1151=EDGE_CURVE ( 'NONE', #6853, #4502, #11242, .T. ) ;
#1153=ORIENTED_EDGE ( 'NONE', *, *, #976, .T. ) ;
#1162=VERTEX_POINT ( 'NONE', #5716 ) ;
#1175=DIRECTION ( 'NONE',  ( 0.000000000000000000, 0.000000000000000000, 1.000000000000000000 ) ) ;
#1180=( LENGTH_UNIT ( ) NAMED_UNIT ( * ) SI_UNIT ( .MILLI., .METRE. ) );
#1183=DIRECTION ( 'NONE',  ( 0.000000000000000000, -6.982962677686266711E-15, 1.000000000000000000 ) ) ;
#1187=VERTEX_POINT ( 'NONE', #7045 ) ;
#1196=CIRCLE ( 'NONE', #11825, 33.00000000003299760 ) ;
#1199=VECTOR ( 'NONE', #14595, 1000.000000000000000 ) ;
#1200=DIRECTION ( 'NONE',  ( 0.000000000000000000, 0.000000000000000000, 1.000000000000000000 ) ) ;
#1223=AXIS2_PLACEMENT_3D ( 'NONE', #10505, #17666, #3379 ) ;
#1227=DIRECTION ( 'NONE',  ( -1.000000000000000000, -0.000000000000000000, 0.000000000000000000 ) ) ;
#1230=CARTESIAN_POINT ( 'NONE',  ( 10.00000000000000178, 0.000000000000000000, 0.000000000000000000 ) ) ;
#1232=ORIENTED_EDGE ( 'NONE', *, *, #1897, .T. ) ;
#1251=DIRECTION ( 'NONE',  ( -1.000000000000000000, 0.000000000000000000, -0.000000000000000000 ) ) ;
#1265=ORIENTED_EDGE ( 'NONE', *, *, #16333, .T. ) ;
#1266=ORIENTED_EDGE ( 'NONE', *, *, #17499, .F. ) ;
#1271=LINE ( 'NONE', #7065, #7548 ) ;
#1273=EDGE_CURVE ( 'NONE', #15756, #13213, #11787, .T. ) ;
#1278=DIRECTION ( 'NONE',  ( 1.000000000000000000, -0.000000000000000000, -0.000000000000000000 ) ) ;
#1283=PRODUCT_CONTEXT ( 'NONE', #13155, 'mechanical' ) ;
#1290=CYLINDRICAL_SURFACE ( 'NONE', #17578, 33.00000000003299760 ) ;
#1295=VERTEX_POINT ( 'NONE', #2169 ) ;
#1302=LINE ( 'NONE', #13013, #5341 ) ;
#1304=VERTEX_POINT ( 'NONE', #7975 ) ;
#1308=EDGE_CURVE ( 'NONE', #12068, #9105, #850, .T. ) ;
#1309=AXIS2_PLACEMENT_3D ( 'NONE', #14116, #10877, #5169 ) ;
#1312=ORIENTED_EDGE ( 'NONE', *, *, #2507, .T. ) ;
#1321=ORIENTED_EDGE ( 'NONE', *, *, #3129, .T. ) ;
#1323=CARTESIAN_POINT ( 'NONE',  ( 5.000000000000000000, 15.68049343256038419, -29.03656532225546627 ) ) ;
#1338=DIRECTION ( 'NONE',  ( 0.000000000000000000, -0.3090169943749548342, 0.9510565162951511997 ) ) ;
#1340=DIRECTION ( 'NONE',  ( 0.000000000000000000, 0.3090169943749411785, 0.9510565162951556406 ) ) ;
#1355=CARTESIAN_POINT ( 'NONE',  ( 0.000000000000000000, -24.46385708179976604, -9.514709542737152859 ) ) ;
#1356=ORIENTED_EDGE ( 'NONE', *, *, #2247, .T. ) ;
#1357=ADVANCED_FACE ( 'NONE', ( #2542 ), #6031, .T. ) ;
#1358=LINE ( 'NONE', #15552, #15713 ) ;
#1366=VERTEX_POINT ( 'NONE', #10412 ) ;
#1375=LINE ( 'NONE', #13181, #2373 ) ;
#1381=DIRECTION ( 'NONE',  ( -1.000000000000000000, -0.000000000000000000, -0.000000000000000000 ) ) ;
#1385=ORIENTED_EDGE ( 'NONE', *, *, #9563, .T. ) ;
#1391=EDGE_CURVE ( 'NONE', #7353, #14282, #5087, .T. ) ;
#1392=CARTESIAN_POINT ( 'NONE',  ( 0.000000000000000000, -1.489278925039700052, 26.20671763660628173 ) ) ;
#1394=CARTESIAN_POINT ( 'NONE',  ( 10.00000000000000000, 26.20671763660628528, -1.489278925039611901 ) ) ;
#1399=ORIENTED_EDGE ( 'NONE', *, *, #3782, .T. ) ;
#1401=ORIENTED_EDGE ( 'NONE', *, *, #12750, .T. ) ;
#1406=EDGE_LOOP ( 'NONE', ( #9767, #18125, #1265, #12186 ) ) ;
#1419=ORIENTED_EDGE ( 'NONE', *, *, #447, .F. ) ;
#1420=CARTESIAN_POINT ( 'NONE',  ( 10.00000000000000000, 24.79895094899259789, 13.40641754777674421 ) ) ;
#1426=DIRECTION ( 'NONE',  ( -1.000000000000000000, 0.000000000000000000, 0.000000000000000000 ) ) ;
#1434=ADVANCED_FACE ( 'NONE', ( #13274 ), #17042, .T. ) ;
#1439=AXIS2_PLACEMENT_3D ( 'NONE', #1230, #16844, #18268 ) ;
#1441=ORIENTED_EDGE ( 'NONE', *, *, #14547, .F. ) ;
#1448=VECTOR ( 'NONE', #16372, 1000.000000000000000 ) ;
#1450=CARTESIAN_POINT ( 'NONE',  ( 0.000000000000000000, -9.514709542737069370, 24.46385708179980512 ) ) ;
#1455=CARTESIAN_POINT ( 'NONE',  ( 10.00000000000000000, 0.000000000000000000, 0.000000000000000000 ) ) ;
#1467=ORIENTED_EDGE ( 'NONE', *, *, #1019, .T. ) ;
#1468=AXIS2_PLACEMENT_3D ( 'NONE', #18555, #9500, #6546 ) ;
#1472=VECTOR ( 'NONE', #774, 1000.000000000000000 ) ;
#1481=DIRECTION ( 'NONE',  ( 0.000000000000000000, 0.5877852522924741363, -0.8090169943749465631 ) ) ;
#1483=DIRECTION ( 'NONE',  ( 0.000000000000000000, 0.000000000000000000, 1.000000000000000000 ) ) ;
#1497=DIRECTION ( 'NONE',  ( 0.000000000000000000, 1.000000000000000000, 3.469446951950143595E-15 ) ) ;
#1505=AXIS2_PLACEMENT_3D ( 'NONE', #11559, #6881, #12702 ) ;
#1517=ORIENTED_EDGE ( 'NONE', *, *, #17830, .T. ) ;
#1523=DIRECTION ( 'NONE',  ( -1.000000000000000000, 0.000000000000000000, 0.000000000000000000 ) ) ;
#1528=CYLINDRICAL_SURFACE ( 'NONE', #2024, 5.000000000000000000 ) ;
#1535=ADVANCED_FACE ( 'NONE', ( #3275 ), #6125, .T. ) ;
#1544=DIRECTION ( 'NONE',  ( -1.000000000000000000, -0.000000000000000000, 0.000000000000000000 ) ) ;
#1548=CARTESIAN_POINT ( 'NONE',  ( 10.00000000000000000, -6.681932690256794594, -25.38428207620328791 ) ) ;
#1550=CARTESIAN_POINT ( 'NONE',  ( 10.00000000000000000, -22.07705612348828694, -14.19907017806892569 ) ) ;
#1560=CYLINDRICAL_SURFACE ( 'NONE', #11255, 12.00000000001200462 ) ;
#1563=ADVANCED_FACE ( 'NONE', ( #7644 ), #6216, .T. ) ;
#1569=AXIS2_PLACEMENT_3D ( 'NONE', #16065, #4538, #4625 ) ;
#1571=CARTESIAN_POINT ( 'NONE',  ( -10.00000000000000000, 0.000000000000000000, 0.000000000000000000 ) ) ;
#1572=CYLINDRICAL_SURFACE ( 'NONE', #10340, 12.00000000001200817 ) ;
#1578=EDGE_LOOP ( 'NONE', ( #10752, #1617, #6248, #8159 ) ) ;
#1586=DIRECTION ( 'NONE',  ( 0.000000000000000000, 0.000000000000000000, -1.000000000000000000 ) ) ;
#1603=ORIENTED_EDGE ( 'NONE', *, *, #2146, .F. ) ;
#1611=DIRECTION ( 'NONE',  ( -1.000000000000000000, -0.000000000000000000, -0.000000000000000000 ) ) ;
#1613=DIRECTION ( 'NONE',  ( -1.000000000000000000, 0.000000000000000000, 0.000000000000000000 ) ) ;
#1615=DIRECTION ( 'NONE',  ( 1.000000000000000000, 0.000000000000000000, 0.000000000000000000 ) ) ;
#1616=DIRECTION ( 'NONE',  ( 0.000000000000000000, 0.000000000000000000, 1.000000000000000000 ) ) ;
#1617=ORIENTED_EDGE ( 'NONE', *, *, #14824, .T. ) ;
#1618=DIRECTION ( 'NONE',  ( 1.000000000000000000, -0.000000000000000000, -0.000000000000000000 ) ) ;
#1619=FACE_OUTER_BOUND ( 'NONE', #15171, .T. ) ;
#1621=AXIS2_PLACEMENT_3D ( 'NONE', #12912, #18712, #5672 ) ;
#1622=ORIENTED_EDGE ( 'NONE', *, *, #447, .T. ) ;
#1625=LINE ( 'NONE', #11725, #320 ) ;
#1627=CARTESIAN_POINT ( 'NONE',  ( 10.00000000000000000, 32.46095361140692859, 5.940243314904329885 ) ) ;
#1628=CARTESIAN_POINT ( 'NONE',  ( 10.00000000000000000, 0.000000000000000000, 0.000000000000000000 ) ) ;
#1630=DIRECTION ( 'NONE',  ( 0.000000000000000000, -0.8090169943749401238, -0.5877852522924831291 ) ) ;
#1632=CARTESIAN_POINT ( 'NONE',  ( 0.000000000000000000, 22.07705612348859958, -14.19907017806844252 ) ) ;
#1636=ORIENTED_EDGE ( 'NONE', *, *, #1042, .T. ) ;
#1638=ORIENTED_EDGE ( 'NONE', *, *, #5200, .T. ) ;
#1640=CYLINDRICAL_SURFACE ( 'NONE', #9296, 5.000000000000000000 ) ;
#1651=CARTESIAN_POINT ( 'NONE',  ( 10.00000000000000000, 9.514709542737238124, -24.46385708179973406 ) ) ;
#1662=ORIENTED_EDGE ( 'NONE', *, *, #10152, .T. ) ;
#1663=CIRCLE ( 'NONE', #12299, 12.00000000001200284 ) ;
#1669=ORIENTED_EDGE ( 'NONE', *, *, #6473, .F. ) ;
#1672=AXIS2_PLACEMENT_3D ( 'NONE', #3878, #2251, #11206 ) ;
#1682=CARTESIAN_POINT ( 'NONE',  ( 0.000000000000000000, -20.32630374611196800, 16.60877409751161693 ) ) ;
#1687=EDGE_CURVE ( 'NONE', #7353, #5299, #3597, .T. ) ;
#1694=FACE_OUTER_BOUND ( 'NONE', #14322, .T. ) ;
#1712=VECTOR ( 'NONE', #637, 1000.000000000000000 ) ;
#1719=DIRECTION ( 'NONE',  ( -1.000000000000000000, -0.000000000000000000, -0.000000000000000000 ) ) ;
#1722=DIRECTION ( 'NONE',  ( 1.000000000000000000, -0.000000000000000000, 0.000000000000000000 ) ) ;
#1736=CIRCLE ( 'NONE', #13603, 26.24900000002624978 ) ;
#1740=VECTOR ( 'NONE', #534, 1000.000000000000000 ) ;
#1748=ORIENTED_EDGE ( 'NONE', *, *, #2896, .F. ) ;
#1751=CARTESIAN_POINT ( 'NONE',  ( 10.00000000000000000, 9.514709542736897063, 24.46385708179987262 ) ) ;
#1786=CIRCLE ( 'NONE', #5129, 26.24900000002624978 ) ;
#1789=CIRCLE ( 'NONE', #7867, 12.00000000001200107 ) ;
#1794=AXIS2_PLACEMENT_3D ( 'NONE', #6987, #12798, #18601 ) ;
#1800=DIRECTION ( 'NONE',  ( 0.000000000000000000, 0.000000000000000000, 1.000000000000000000 ) ) ;
#1801=EDGE_CURVE ( 'NONE', #3758, #1187, #18490, .T. ) ;
#1821=AXIS2_PLACEMENT_3D ( 'NONE', #7093, #17200, #1483 ) ;
#1824=EDGE_LOOP ( 'NONE', ( #12807, #16818, #6158, #5332 ) ) ;
#1830=ORIENTED_EDGE ( 'NONE', *, *, #2896, .T. ) ;
#1847=FACE_OUTER_BOUND ( 'NONE', #14781, .T. ) ;
#1849=ORIENTED_EDGE ( 'NONE', *, *, #7423, .T. ) ;
#1860=ORIENTED_EDGE ( 'NONE', *, *, #9882, .F. ) ;
#1863=EDGE_CURVE ( 'NONE', #7974, #5783, #14590, .T. ) ;
#1865=CARTESIAN_POINT ( 'NONE',  ( 10.00000000000000000, 0.000000000000000000, 0.000000000000000000 ) ) ;
#1866=ORIENTED_EDGE ( 'NONE', *, *, #6568, .F. ) ;
#1873=EDGE_LOOP ( 'NONE', ( #7692, #16429, #13707, #86 ) ) ;
#1884=ORIENTED_EDGE ( 'NONE', *, *, #7990, .F. ) ;
#1895=DIRECTION ( 'NONE',  ( -1.000000000000000000, 0.000000000000000000, 0.000000000000000000 ) ) ;
#1897=EDGE_CURVE ( 'NONE', #11652, #6251, #5412, .T. ) ;
#1901=AXIS2_PLACEMENT_3D ( 'NONE', #17050, #952, #6747 ) ;
#1903=AXIS2_PLACEMENT_3D ( 'NONE', #7837, #14987, #10413 ) ;
#1904=EDGE_CURVE ( 'NONE', #9105, #364, #4396, .T. ) ;
#1913=ORIENTED_EDGE ( 'NONE', *, *, #8065, .T. ) ;
#1914=CARTESIAN_POINT ( 'NONE',  ( 50.00005079999999680, 4.769696007084728073, 1.500000000000000000 ) ) ;
#1915=ORIENTED_EDGE ( 'NONE', *, *, #7281, .F. ) ;
#1917=FACE_OUTER_BOUND ( 'NONE', #17047, .T. ) ;
#1923=CIRCLE ( 'NONE', #13489, 12.00000000001200284 ) ;
#1927=DIRECTION ( 'NONE',  ( -1.000000000000000000, -0.000000000000000000, 0.000000000000000000 ) ) ;
#1930=AXIS2_PLACEMENT_3D ( 'NONE', #236, #16513, #2130 ) ;
#1936=EDGE_LOOP ( 'NONE', ( #17912, #8400, #3142, #14656 ) ) ;
#1952=ORIENTED_EDGE ( 'NONE', *, *, #3368, .T. ) ;
#1954=DIRECTION ( 'NONE',  ( 0.000000000000000000, 0.000000000000000000, 1.000000000000000000 ) ) ;
#1957=STYLED_ITEM ( 'NONE', ( #14929 ), #6260 ) ;
#1964=FILL_AREA_STYLE ('',( #7964 ) ) ;
#1965=VERTEX_POINT ( 'NONE', #14767 ) ;
#1967=EDGE_CURVE ( 'NONE', #9230, #13703, #12285, .T. ) ;
#1970=VECTOR ( 'NONE', #14156, 1000.000000000000000 ) ;
#1975=DIRECTION ( 'NONE',  ( 0.000000000000000000, 0.3090169943749410120, 0.9510565162951556406 ) ) ;
#1978=DIRECTION ( 'NONE',  ( -1.000000000000000000, -0.000000000000000000, -0.000000000000000000 ) ) ;
#1985=AXIS2_PLACEMENT_3D ( 'NONE', #5269, #6614, #16805 ) ;
#1992=VECTOR ( 'NONE', #16512, 1000.000000000000000 ) ;
#1993=ORIENTED_EDGE ( 'NONE', *, *, #14984, .T. ) ;
#1995=CIRCLE ( 'NONE', #7772, 26.24900000002625333 ) ;
#2003=CARTESIAN_POINT ( 'NONE',  ( -10.00000000000000000, 0.000000000000000000, 0.000000000000000000 ) ) ;
#2006=CARTESIAN_POINT ( 'NONE',  ( 0.000000000000000000, -20.32630374611172641, -16.60877409751190470 ) ) ;
#2008=CARTESIAN_POINT ( 'NONE',  ( 0.000000000000000000, 0.000000000000000000, 0.000000000000000000 ) ) ;
#2011=CIRCLE ( 'NONE', #9930, 12.00000000001200817 ) ;
#2016=AXIS2_PLACEMENT_3D ( 'NONE', #7448, #14891, #17655 ) ;
#2017=AXIS2_PLACEMENT_3D ( 'NONE', #2176, #758, #3339 ) ;
#2018=EDGE_LOOP ( 'NONE', ( #15909, #13072, #16843, #3478 ) ) ;
#2024=AXIS2_PLACEMENT_3D ( 'NONE', #107, #7136, #11715 ) ;
#2027=ADVANCED_FACE ( 'NONE', ( #13633 ), #585, .T. ) ;
#2037=CYLINDRICAL_SURFACE ( 'NONE', #18207, 12.00000000001200817 ) ;
#2047=CARTESIAN_POINT ( 'NONE',  ( 0.000000000000000000, 23.88582760061481380, 22.76987570971536101 ) ) ;
#2050=AXIS2_PLACEMENT_3D ( 'NONE', #15904, #11709, #2953 ) ;
#2051=AXIS2_PLACEMENT_3D ( 'NONE', #7297, #5869, #8721 ) ;
#2055=CARTESIAN_POINT ( 'NONE',  ( 5.000000000000000000, -14.27431201565546459, 29.75305054077467659 ) ) ;
#2056=ORIENTED_EDGE ( 'NONE', *, *, #17418, .T. ) ;
#2058=AXIS2_PLACEMENT_3D ( 'NONE', #15507, #10926, #18170 ) ;
#2062=CIRCLE ( 'NONE', #7220, 33.00000000003299760 ) ;
#2065=AXIS2_PLACEMENT_3D ( 'NONE', #11479, #2894, #10046 ) ;
#2069=ADVANCED_FACE ( 'NONE', ( #16678 ), #14967, .T. ) ;
#2076=VECTOR ( 'NONE', #14136, 1000.000000000000000 ) ;
#2081=ORIENTED_EDGE ( 'NONE', *, *, #16874, .T. ) ;
#2086=CYLINDRICAL_SURFACE ( 'NONE', #14218, 12.00000000001200817 ) ;
#2090=VECTOR ( 'NONE', #1278, 1000.000000000000000 ) ;
#2092=ORIENTED_EDGE ( 'NONE', *, *, #3782, .F. ) ;
#2100=ORIENTED_EDGE ( 'NONE', *, *, #14263, .T. ) ;
#2105=CARTESIAN_POINT ( 'NONE',  ( -10.00000000000000000, 0.000000000000000000, 0.000000000000000000 ) ) ;
#2110=AXIS2_PLACEMENT_3D ( 'NONE', #11430, #2772, #2862 ) ;
#2112=CIRCLE ( 'NONE', #2734, 26.24900000002625688 ) ;
#2130=DIRECTION ( 'NONE',  ( 0.000000000000000000, 0.000000000000000000, 1.000000000000000000 ) ) ;
#2133=ORIENTED_EDGE ( 'NONE', *, *, #1273, .T. ) ;
#2138=AXIS2_PLACEMENT_3D ( 'NONE', #11658, #8119, #10874 ) ;
#2146=EDGE_CURVE ( 'NONE', #1162, #11016, #8385, .T. ) ;
#2162=EDGE_CURVE ( 'NONE', #8506, #1304, #16965, .T. ) ;
#2168=ORIENTED_EDGE ( 'NONE', *, *, #11210, .F. ) ;
#2169=CARTESIAN_POINT ( 'NONE',  ( 0.000000000000000000, 32.46095361140693569, 5.940243314904326333 ) ) ;
#2172=ORIENTED_EDGE ( 'NONE', *, *, #13675, .T. ) ;
#2176=CARTESIAN_POINT ( 'NONE',  ( 10.00000000000000000, -13.40641754777683126, 24.79895094899255170 ) ) ;
#2186=ORIENTED_EDGE ( 'NONE', *, *, #4002, .F. ) ;
#2192=VECTOR ( 'NONE', #4103, 1000.000000000000000 ) ;
#2195=ORIENTED_EDGE ( 'NONE', *, *, #12960, .T. ) ;
#2217=ORIENTED_EDGE ( 'NONE', *, *, #198, .F. ) ;
#2224=DIRECTION ( 'NONE',  ( 0.000000000000000000, 0.000000000000000000, 1.000000000000000000 ) ) ;
#2231=LINE ( 'NONE', #11283, #2076 ) ;
#2247=EDGE_CURVE ( 'NONE', #5512, #4486, #16682, .T. ) ;
#2248=ORIENTED_EDGE ( 'NONE', *, *, #341, .F. ) ;
#2250=ADVANCED_FACE ( 'NONE', ( #5897 ), #8844, .T. ) ;
#2251=DIRECTION ( 'NONE',  ( -1.000000000000000000, 0.000000000000000000, 0.000000000000000000 ) ) ;
#2255=( GEOMETRIC_REPRESENTATION_CONTEXT ( 3 ) GLOBAL_UNCERTAINTY_ASSIGNED_CONTEXT ( ( #14163 ) ) GLOBAL_UNIT_ASSIGNED_CONTEXT ( ( #3316, #643, #17774 ) ) REPRESENTATION_CONTEXT ( 'NONE', 'WORKASPACE' ) );
#2262=EDGE_CURVE ( 'NONE', #16693, #9892, #11198, .T. ) ;
#2270=DIRECTION ( 'NONE',  ( 0.000000000000000000, 0.000000000000000000, 1.000000000000000000 ) ) ;
#2284=EDGE_LOOP ( 'NONE', ( #2056, #14725, #15450, #18594 ) ) ;
#2287=LINE ( 'NONE', #15337, #3908 ) ;
#2292=EDGE_LOOP ( 'NONE', ( #6465, #3265, #17753, #3454 ) ) ;
#2296=ORIENTED_EDGE ( 'NONE', *, *, #4987, .T. ) ;
#2297=CARTESIAN_POINT ( 'NONE',  ( 10.00000000000000000, 19.44239304137403579, -20.41355805489595454 ) ) ;
#2302=EDGE_CURVE ( 'NONE', #7010, #7125, #16069, .T. ) ;
#2304=CARTESIAN_POINT ( 'NONE',  ( 5.000000000000000000, 32.46095361140693569, 5.940243314904328109 ) ) ;
#2311=EDGE_CURVE ( 'NONE', #15970, #353, #18501, .T. ) ;
#2325=CYLINDRICAL_SURFACE ( 'NONE', #16306, 26.24900000002624978 ) ;
#2328=VECTOR ( 'NONE', #9719, 1000.000000000000000 ) ;
#2330=DIRECTION ( 'NONE',  ( -1.000000000000000000, 0.000000000000000000, 0.000000000000000000 ) ) ;
#2334=DIRECTION ( 'NONE',  ( 0.000000000000000000, 0.000000000000000000, 1.000000000000000000 ) ) ;
#2340=DIRECTION ( 'NONE',  ( -1.000000000000000000, -0.000000000000000000, 0.000000000000000000 ) ) ;
#2347=CARTESIAN_POINT ( 'NONE',  ( 5.000000000000000000, -23.88582760061464327, -22.76987570971553865 ) ) ;
#2349=CIRCLE ( 'NONE', #17867, 33.00000000003299760 ) ;
#2356=CARTESIAN_POINT ( 'NONE',  ( 10.00000000000000000, 24.79895094899259789, 13.40641754777674421 ) ) ;
#2363=CARTESIAN_POINT ( 'NONE',  ( 10.00000000000000000, -24.79895094899250196, -13.40641754777691830 ) ) ;
#2366=EDGE_LOOP ( 'NONE', ( #12175, #4324, #13360, #6401, #3599, #1830, #4859, #11381, #5917, #10798, #7889, #14435, #6870, #2195, #13992, #9394, #7391, #6133, #13256, #3028, #4553, #977, #4853, #12155, #6493, #15310, #6244, #3793, #10062, #8027, #11526, #861, #9036, #5903, #10490, #3546, #12485, #7005, #6649, #1356, #4678, #18808, #11387, #1022, #3314, #8938, #15341, #1113, #11429, #783, #15113, #10313, #4580, #16055, #16529, #1849, #12936, #8649, #13650, #17406, #11669, #14738, #11637, #587, #4304, #14830, #6857, #9441, #18558, #5880, #11416, #5307, #7292, #12744, #13892, #13587, #11400, #10452, #9403, #17096, #6139, #18431, #4031, #9466, #7416 ) ) ;
#2368=ADVANCED_FACE ( 'NONE', ( #17346 ), #7048, .T. ) ;
#2373=VECTOR ( 'NONE', #5928, 1000.000000000000000 ) ;
#2375=EDGE_CURVE ( 'NONE', #7022, #8500, #17317, .T. ) ;
#2377=EDGE_CURVE ( 'NONE', #10560, #1162, #573, .T. ) ;
#2378=AXIS2_PLACEMENT_3D ( 'NONE', #12154, #3304, #1954 ) ;
#2381=CARTESIAN_POINT ( 'NONE',  ( 10.00000000000000000, -27.94286728106395756, 3.730438010304225394 ) ) ;
#2383=EDGE_CURVE ( 'NONE', #16587, #9667, #17428, .T. ) ;
#2389=AXIS2_PLACEMENT_3D ( 'NONE', #16989, #13741, #695 ) ;
#2392=CIRCLE ( 'NONE', #12005, 12.00000000001200817 ) ;
#2414=CARTESIAN_POINT ( 'NONE',  ( 10.00000000000000000, -9.514709542736730086, -24.46385708179992946 ) ) ;
#2416=CARTESIAN_POINT ( 'NONE',  ( 0.000000000000000000, -26.20671763660627462, -1.489278925039791535 ) ) ;
#2418=VECTOR ( 'NONE', #7496, 1000.000000000000000 ) ;
#2425=CARTESIAN_POINT ( 'NONE',  ( 0.000000000000000000, 5.940243314904213534, 32.46095361140695701 ) ) ;
#2429=CARTESIAN_POINT ( 'NONE',  ( 0.000000000000000000, 0.000000000000000000, 0.000000000000000000 ) ) ;
#2441=EDGE_LOOP ( 'NONE', ( #2463, #5836, #1638, #3081 ) ) ;
#2461=DIRECTION ( 'NONE',  ( 0.000000000000000000, 0.000000000000000000, 1.000000000000000000 ) ) ;
#2462=ORIENTED_EDGE ( 'NONE', *, *, #9683, .T. ) ;
#2463=ORIENTED_EDGE ( 'NONE', *, *, #14012, .F. ) ;
#2464=FACE_OUTER_BOUND ( 'NONE', #12003, .T. ) ;
#2470=VERTEX_POINT ( 'NONE', #15035 ) ;
#2478=LINE ( 'NONE', #8295, #2192 ) ;
#2481=DIRECTION ( 'NONE',  ( -1.000000000000000000, 0.000000000000000000, 0.000000000000000000 ) ) ;
#2482=EDGE_CURVE ( 'NONE', #13703, #17590, #4239, .T. ) ;
#2486=EDGE_CURVE ( 'NONE', #1187, #11652, #1789, .T. ) ;
#2489=EDGE_CURVE ( 'NONE', #17607, #15207, #2392, .T. ) ;
#2507=EDGE_CURVE ( 'NONE', #10912, #16587, #3013, .T. ) ;
#2519=CARTESIAN_POINT ( 'NONE',  ( 10.00000000000000000, 0.000000000000000000, 0.000000000000000000 ) ) ;
#2521=CARTESIAN_POINT ( 'NONE',  ( 0.000000000000000000, -5.940243314904443572, 32.46095361140691438 ) ) ;
#2529=CARTESIAN_POINT ( 'NONE',  ( 0.000000000000000000, -27.94286728106395756, 3.730438010304225394 ) ) ;
#2532=CARTESIAN_POINT ( 'NONE',  ( 10.00000000000000000, -9.514709542736730086, -24.46385708179992946 ) ) ;
#2536=CIRCLE ( 'NONE', #1621, 12.00000000001200462 ) ;
#2542=FACE_OUTER_BOUND ( 'NONE', #8712, .T. ) ;
#2545=EDGE_LOOP ( 'NONE', ( #10844, #253, #1321, #75 ) ) ;
#2554=CARTESIAN_POINT ( 'NONE',  ( 10.00000000000000000, -24.79895094899269026, 13.40641754777657013 ) ) ;
#2571=CARTESIAN_POINT ( 'NONE',  ( 10.00000000000000000, 27.94286728106393269, 3.730438010304423013 ) ) ;
#2575=AXIS2_PLACEMENT_3D ( 'NONE', #9026, #13329, #16266 ) ;
#2577=EDGE_LOOP ( 'NONE', ( #2866, #8006, #16344, #3214 ) ) ;
#2585=CIRCLE ( 'NONE', #4407, 12.00000000001200462 ) ;
#2608=EDGE_CURVE ( 'NONE', #923, #17584, #18270, .T. ) ;
#2614=CARTESIAN_POINT ( 'NONE',  ( 10.00000000000000000, 0.000000000000000000, 0.000000000000000000 ) ) ;
#2617=CARTESIAN_POINT ( 'NONE',  ( 5.000000000000000000, 14.27431201565567243, -29.75305054077457356 ) ) ;
#2618=CIRCLE ( 'NONE', #15396, 12.00000000001200817 ) ;
#2623=FACE_OUTER_BOUND ( 'NONE', #13642, .T. ) ;
#2624=EDGE_LOOP ( 'NONE', ( #8240, #18567, #14708, #5265 ) ) ;
#2651=VECTOR ( 'NONE', #16286, 1000.000000000000000 ) ;
#2656=ORIENTED_EDGE ( 'NONE', *, *, #10515, .T. ) ;
#2663=AXIS2_PLACEMENT_3D ( 'NONE', #5595, #18553, #16228 ) ;
#2664=ORIENTED_EDGE ( 'NONE', *, *, #3537, .T. ) ;
#2667=ORIENTED_EDGE ( 'NONE', *, *, #8550, .F. ) ;
#2673=CARTESIAN_POINT ( 'NONE',  ( 0.000000000000000000, 0.000000000000000000, 0.000000000000000000 ) ) ;
#2681=EDGE_LOOP ( 'NONE', ( #9489, #3434, #9838, #1517 ) ) ;
#2688=CIRCLE ( 'NONE', #9668, 26.24900000002625688 ) ;
#2689=ADVANCED_FACE ( 'NONE', ( #15416 ), #17049, .T. ) ;
#2693=AXIS2_PLACEMENT_3D ( 'NONE', #13, #1611, #13145 ) ;
#2701=DIRECTION ( 'NONE',  ( 0.000000000000000000, 0.000000000000000000, 1.000000000000000000 ) ) ;
#2704=EDGE_CURVE ( 'NONE', #14291, #2833, #9792, .T. ) ;
#2708=EDGE_CURVE ( 'NONE', #9496, #8847, #13648, .T. ) ;
#2712=EDGE_CURVE ( 'NONE', #8620, #8889, #1196, .T. ) ;
#2713=DIRECTION ( 'NONE',  ( 1.000000000000000000, 0.000000000000000000, -0.000000000000000000 ) ) ;
#2718=AXIS2_PLACEMENT_3D ( 'NONE', #2844, #15517, #9799 ) ;
#2734=AXIS2_PLACEMENT_3D ( 'NONE', #7834, #793, #12213 ) ;
#2772=DIRECTION ( 'NONE',  ( -1.000000000000000000, -0.000000000000000000, -0.000000000000000000 ) ) ;
#2789=FACE_OUTER_BOUND ( 'NONE', #15795, .T. ) ;
#2792=ORIENTED_EDGE ( 'NONE', *, *, #270, .T. ) ;
#2809=EDGE_LOOP ( 'NONE', ( #7698, #6529, #4423, #498 ) ) ;
#2813=FACE_OUTER_BOUND ( 'NONE', #12249, .T. ) ;
#2814=ORIENTED_EDGE ( 'NONE', *, *, #6913, .F. ) ;
#2822=VECTOR ( 'NONE', #1032, 1000.000000000000000 ) ;
#2826=ORIENTED_EDGE ( 'NONE', *, *, #5762, .F. ) ;
#2833=VERTEX_POINT ( 'NONE', #17327 ) ;
#2836=CARTESIAN_POINT ( 'NONE',  ( 10.00000000000000000, 0.000000000000000000, 0.000000000000000000 ) ) ;
#2844=CARTESIAN_POINT ( 'NONE',  ( 10.00000000000000000, 27.72801475327282361, -5.086963483077305170 ) ) ;
#2855=FACE_OUTER_BOUND ( 'NONE', #14001, .T. ) ;
#2858=CARTESIAN_POINT ( 'NONE',  ( 10.00000000000000000, 0.000000000000000000, 0.000000000000000000 ) ) ;
#2862=DIRECTION ( 'NONE',  ( 0.000000000000000000, 0.000000000000000000, 1.000000000000000000 ) ) ;
#2865=EDGE_CURVE ( 'NONE', #9332, #13562, #14637, .T. ) ;
#2866=ORIENTED_EDGE ( 'NONE', *, *, #2302, .F. ) ;
#2894=DIRECTION ( 'NONE',  ( -1.000000000000000000, 0.000000000000000000, 0.000000000000000000 ) ) ;
#2896=EDGE_CURVE ( 'NONE', #12127, #7525, #12044, .T. ) ;
#2897=CARTESIAN_POINT ( 'NONE',  ( 10.00000000000000000, -16.60877409751182654, 20.32630374611179391 ) ) ;
#2898=ORIENTED_EDGE ( 'NONE', *, *, #3368, .F. ) ;
#2902=FACE_OUTER_BOUND ( 'NONE', #17979, .T. ) ;
#2906=ORIENTED_EDGE ( 'NONE', *, *, #5226, .F. ) ;
#2912=CARTESIAN_POINT ( 'NONE',  ( 0.000000000000000000, 0.000000000000000000, 0.000000000000000000 ) ) ;
#2914=DIRECTION ( 'NONE',  ( -1.000000000000000000, 0.000000000000000000, 0.000000000000000000 ) ) ;
#2933=CIRCLE ( 'NONE', #16607, 26.24900000002625333 ) ;
#2950=DIRECTION ( 'NONE',  ( -1.000000000000000000, -0.000000000000000000, 0.000000000000000000 ) ) ;
#2953=DIRECTION ( 'NONE',  ( 0.000000000000000000, -0.8090169943749532244, 0.5877852522924652545 ) ) ;
#2955=CARTESIAN_POINT ( 'NONE',  ( 10.00000000000000000, 0.000000000000000000, 0.000000000000000000 ) ) ;
#2962=CARTESIAN_POINT ( 'NONE',  ( 0.000000000000000000, 27.72801475327282361, -5.086963483077305170 ) ) ;
#2965=ADVANCED_FACE ( 'NONE', ( #12156 ), #4916, .T. ) ;
#2970=ADVANCED_FACE ( 'NONE', ( #3592 ), #731, .T. ) ;
#2980=EDGE_CURVE ( 'NONE', #10448, #12127, #6441, .T. ) ;
#2994=AXIS2_PLACEMENT_3D ( 'NONE', #4913, #9192, #6242 ) ;
#3004=DIRECTION ( 'NONE',  ( -1.000000000000000000, 0.000000000000000000, 0.000000000000000000 ) ) ;
#3006=CIRCLE ( 'NONE', #17900, 12.00000000001200640 ) ;
#3008=DIRECTION ( 'NONE',  ( 0.000000000000000000, 0.000000000000000000, 1.000000000000000000 ) ) ;
#3013=CIRCLE ( 'NONE', #18523, 26.24900000002625688 ) ;
#3028=ORIENTED_EDGE ( 'NONE', *, *, #6845, .T. ) ;
#3031=ORIENTED_EDGE ( 'NONE', *, *, #9947, .F. ) ;
#3032=ORIENTED_EDGE ( 'NONE', *, *, #15524, .F. ) ;
#3036=( NAMED_UNIT ( * ) PLANE_ANGLE_UNIT ( ) SI_UNIT ( $, .RADIAN. ) );
#3037=ORIENTED_EDGE ( 'NONE', *, *, #681, .T. ) ;
#3039=EDGE_CURVE ( 'NONE', #6042, #6241, #12334, .T. ) ;
#3040=CYLINDRICAL_SURFACE ( 'NONE', #4626, 33.00000000003299760 ) ;
#3044=EDGE_LOOP ( 'NONE', ( #1083, #17491, #12330, #6547 ) ) ;
#3046=CARTESIAN_POINT ( 'NONE',  ( 10.00000000000000000, -6.681932690256794594, -25.38428207620328791 ) ) ;
#3049=CARTESIAN_POINT ( 'NONE',  ( 10.00000000000000000, 16.60877409751197575, -20.32630374611166957 ) ) ;
#3050=DIRECTION ( 'NONE',  ( 1.000000000000000000, 0.000000000000000000, 0.000000000000000000 ) ) ;
#3055=DIRECTION ( 'NONE',  ( 0.000000000000000000, -6.938893903900287191E-15, 1.000000000000000000 ) ) ;
#3074=DIRECTION ( 'NONE',  ( 1.000000000000000000, -0.000000000000000000, 0.000000000000000000 ) ) ;
#3075=ORIENTED_EDGE ( 'NONE', *, *, #5533, .T. ) ;
#3076=CARTESIAN_POINT ( 'NONE',  ( 10.00000000000000000, -25.38428207620327370, 6.681932690256871865 ) ) ;
#3081=ORIENTED_EDGE ( 'NONE', *, *, #6072, .T. ) ;
#3094=ORIENTED_EDGE ( 'NONE', *, *, #18434, .T. ) ;
#3098=CARTESIAN_POINT ( 'NONE',  ( 10.00000000000000000, 23.88582760061481380, 22.76987570971535746 ) ) ;
#3101=EDGE_CURVE ( 'NONE', #4267, #14062, #5056, .T. ) ;
#3110=CARTESIAN_POINT ( 'NONE',  ( 0.000000000000000000, -5.086963483077008519, -27.72801475327286980 ) ) ;
#3111=ORIENTED_EDGE ( 'NONE', *, *, #18029, .F. ) ;
#3119=ORIENTED_EDGE ( 'NONE', *, *, #5107, .F. ) ;
#3122=( NAMED_UNIT ( * ) SI_UNIT ( $, .STERADIAN. ) SOLID_ANGLE_UNIT ( ) );
#3129=EDGE_CURVE ( 'NONE', #6635, #12242, #5367, .T. ) ;
#3135=VERTEX_POINT ( 'NONE', #17304 ) ;
#3142=ORIENTED_EDGE ( 'NONE', *, *, #6093, .T. ) ;
#3145=FACE_OUTER_BOUND ( 'NONE', #18317, .T. ) ;
#3146=VERTEX_POINT ( 'NONE', #9768 ) ;
#3147=CARTESIAN_POINT ( 'NONE',  ( 0.000000000000000000, 19.44239304137403579, -20.41355805489595454 ) ) ;
#3155=DIRECTION ( 'NONE',  ( 0.000000000000000000, 0.000000000000000000, 1.000000000000000000 ) ) ;
#3169=VERTEX_POINT ( 'NONE', #15578 ) ;
#3171=DIRECTION ( 'NONE',  ( 0.000000000000000000, 0.5877852522924686962, 0.8090169943749507819 ) ) ;
#3173=DIRECTION ( 'NONE',  ( 1.000000000000000000, 0.000000000000000000, 0.000000000000000000 ) ) ;
#3179=DIRECTION ( 'NONE',  ( -1.000000000000000000, -0.000000000000000000, 0.000000000000000000 ) ) ;
#3203=DIRECTION ( 'NONE',  ( -1.000000000000000000, -0.000000000000000000, 0.000000000000000000 ) ) ;
#3204=CIRCLE ( 'NONE', #8668, 26.24900000002624978 ) ;
#3206=DIRECTION ( 'NONE',  ( 0.000000000000000000, 0.3090169943749479509, -0.9510565162951533091 ) ) ;
#3207=CIRCLE ( 'NONE', #8063, 5.000000000000000000 ) ;
#3214=ORIENTED_EDGE ( 'NONE', *, *, #8068, .T. ) ;
#3215=CARTESIAN_POINT ( 'NONE',  ( 10.00000000000000000, -25.38428207620317778, -6.681932690257235130 ) ) ;
#3219=DIRECTION ( 'NONE',  ( 0.000000000000000000, -1.000000000000000000, -1.047444401652940164E-14 ) ) ;
#3235=CARTESIAN_POINT ( 'NONE',  ( 0.000000000000000000, -13.40641754777683126, 24.79895094899255170 ) ) ;
#3236=AXIS2_PLACEMENT_3D ( 'NONE', #17111, #13547, #11484 ) ;
#3239=DIRECTION ( 'NONE',  ( -1.000000000000000000, 0.000000000000000000, -0.000000000000000000 ) ) ;
#3245=ORIENTED_EDGE ( 'NONE', *, *, #14824, .F. ) ;
#3254=ORIENTED_EDGE ( 'NONE', *, *, #7254, .F. ) ;
#3257=CIRCLE ( 'NONE', #14206, 12.00000000001200462 ) ;
#3265=ORIENTED_EDGE ( 'NONE', *, *, #7721, .F. ) ;
#3266=AXIS2_PLACEMENT_3D ( 'NONE', #10092, #8654, #16991 ) ;
#3268=CIRCLE ( 'NONE', #4774, 33.00000000003299760 ) ;
#3271=VECTOR ( 'NONE', #2914, 1000.000000000000000 ) ;
#3275=FACE_OUTER_BOUND ( 'NONE', #10621, .T. ) ;
#3277=DIRECTION ( 'NONE',  ( 0.000000000000000000, 0.000000000000000000, 1.000000000000000000 ) ) ;
#3280=EDGE_CURVE ( 'NONE', #1091, #16517, #16323, .T. ) ;
#3281=CARTESIAN_POINT ( 'NONE',  ( 10.00000000000000000, -3.730438010304114371, -27.94286728106396822 ) ) ;
#3291=CIRCLE ( 'NONE', #7242, 26.24900000002624978 ) ;
#3294=DIRECTION ( 'NONE',  ( 0.000000000000000000, 0.000000000000000000, -1.000000000000000000 ) ) ;
#3295=CARTESIAN_POINT ( 'NONE',  ( 0.000000000000000000, 3.730438010304726770, -27.94286728106388296 ) ) ;
#3296=CIRCLE ( 'NONE', #4214, 26.24900000002625333 ) ;
#3301=CIRCLE ( 'NONE', #2389, 33.00000000003299760 ) ;
#3304=DIRECTION ( 'NONE',  ( -1.000000000000000000, 0.000000000000000000, 0.000000000000000000 ) ) ;
#3305=VERTEX_POINT ( 'NONE', #17470 ) ;
#3314=ORIENTED_EDGE ( 'NONE', *, *, #8076, .F. ) ;
#3316=( LENGTH_UNIT ( ) NAMED_UNIT ( * ) SI_UNIT ( .MILLI., .METRE. ) );
#3317=ADVANCED_FACE ( 'NONE', ( #10233 ), #12025, .T. ) ;
#3323=CIRCLE ( 'NONE', #8189, 12.00000000001200284 ) ;
#3325=EDGE_CURVE ( 'NONE', #10104, #7022, #12343, .T. ) ;
#3326=CARTESIAN_POINT ( 'NONE',  ( 10.00000000000000000, 0.000000000000000000, 0.000000000000000000 ) ) ;
#3329=ORIENTED_EDGE ( 'NONE', *, *, #11324, .F. ) ;
#3339=DIRECTION ( 'NONE',  ( 0.000000000000000000, 0.000000000000000000, 1.000000000000000000 ) ) ;
#3341=DIRECTION ( 'NONE',  ( 0.000000000000000000, 0.000000000000000000, -1.000000000000000000 ) ) ;
#3342=CARTESIAN_POINT ( 'NONE',  ( 10.00000000000000000, -27.94286728106395756, 3.730438010304225394 ) ) ;
#3368=EDGE_CURVE ( 'NONE', #6276, #8847, #8392, .T. ) ;
#3371=DIRECTION ( 'NONE',  ( -1.000000000000000000, 0.000000000000000000, -0.000000000000000000 ) ) ;
#3378=CYLINDRICAL_SURFACE ( 'NONE', #9842, 12.00000000001200640 ) ;
#3379=DIRECTION ( 'NONE',  ( 0.000000000000000000, 0.000000000000000000, 1.000000000000000000 ) ) ;
#3380=ORIENTED_EDGE ( 'NONE', *, *, #7272, .T. ) ;
#3381=ORIENTED_EDGE ( 'NONE', *, *, #7118, .F. ) ;
#3383=AXIS2_PLACEMENT_3D ( 'NONE', #8267, #942, #18351 ) ;
#3389=CARTESIAN_POINT ( 'NONE',  ( 5.000000000000000000, 29.75305054077472633, 14.27431201565535979 ) ) ;
#3390=EDGE_LOOP ( 'NONE', ( #128, #14960, #7663, #3037 ) ) ;
#3400=ORIENTED_EDGE ( 'NONE', *, *, #681, .F. ) ;
#3405=FACE_OUTER_BOUND ( 'NONE', #2624, .T. ) ;
#3420=EDGE_CURVE ( 'NONE', #514, #16495, #6969, .T. ) ;
#3424=ORIENTED_EDGE ( 'NONE', *, *, #15143, .F. ) ;
#3425=DIRECTION ( 'NONE',  ( 0.000000000000000000, 0.9510565162951523099, 0.3090169943749516701 ) ) ;
#3431=DIRECTION ( 'NONE',  ( 0.000000000000000000, 0.000000000000000000, -1.000000000000000000 ) ) ;
#3434=ORIENTED_EDGE ( 'NONE', *, *, #9228, .T. ) ;
#3436=CARTESIAN_POINT ( 'NONE',  ( 10.00000000000000000, -25.42247726998023083, 12.18267823974742470 ) ) ;
#3437=CIRCLE ( 'NONE', #9204, 26.24900000002625333 ) ;
#3438=ORIENTED_EDGE ( 'NONE', *, *, #11471, .F. ) ;
#3454=ORIENTED_EDGE ( 'NONE', *, *, #2712, .T. ) ;
#3457=DIRECTION ( 'NONE',  ( -1.000000000000000000, -0.000000000000000000, 0.000000000000000000 ) ) ;
#3466=DIRECTION ( 'NONE',  ( -1.000000000000000000, -0.000000000000000000, -0.000000000000000000 ) ) ;
#3469=ORIENTED_EDGE ( 'NONE', *, *, #3325, .F. ) ;
#3470=DIRECTION ( 'NONE',  ( -1.000000000000000000, 0.000000000000000000, 0.000000000000000000 ) ) ;
#3478=ORIENTED_EDGE ( 'NONE', *, *, #8812, .T. ) ;
#3486=VERTEX_POINT ( 'NONE', #5541 ) ;
#3487=PLANE ( 'NONE',  #13336 ) ;
#3488=VERTEX_POINT ( 'NONE', #16971 ) ;
#3498=EDGE_CURVE ( 'NONE', #15207, #34, #2011, .T. ) ;
#3511=DIRECTION ( 'NONE',  ( 0.000000000000000000, 0.8090169943749487835, -0.5877852522924713607 ) ) ;
#3521=VECTOR ( 'NONE', #1722, 1000.000000000000000 ) ;
#3522=ADVANCED_FACE ( 'NONE', ( #3145 ), #7331, .T. ) ;
#3523=AXIS2_PLACEMENT_3D ( 'NONE', #17027, #10809, #5291 ) ;
#3526=EDGE_CURVE ( 'NONE', #2833, #9630, #18454, .T. ) ;
#3527=AXIS2_PLACEMENT_3D ( 'NONE', #10794, #17012, #9660 ) ;
#3529=DIRECTION ( 'NONE',  ( -1.000000000000000000, 0.000000000000000000, 0.000000000000000000 ) ) ;
#3531=CARTESIAN_POINT ( 'NONE',  ( 0.000000000000000000, -24.79895094899250196, -13.40641754777691830 ) ) ;
#3537=EDGE_CURVE ( 'NONE', #6583, #16274, #15410, .T. ) ;
#3546=ORIENTED_EDGE ( 'NONE', *, *, #10293, .T. ) ;
#3549=ADVANCED_FACE ( 'NONE', ( #18767 ), #1528, .F. ) ;
#3552=ADVANCED_FACE ( 'NONE', ( #10010 ), #5902, .T. ) ;
#3558=CARTESIAN_POINT ( 'NONE',  ( -10.00000000000000000, 0.000000000000000000, 0.000000000000000000 ) ) ;
#3566=ORIENTED_EDGE ( 'NONE', *, *, #16168, .F. ) ;
#3588=CIRCLE ( 'NONE', #14236, 26.24900000002624978 ) ;
#3591=ORIENTED_EDGE ( 'NONE', *, *, #5862, .F. ) ;
#3592=FACE_OUTER_BOUND ( 'NONE', #5057, .T. ) ;
#3597=CIRCLE ( 'NONE', #18186, 26.24900000002624978 ) ;
#3599=ORIENTED_EDGE ( 'NONE', *, *, #12856, .T. ) ;
#3605=( GEOMETRIC_REPRESENTATION_CONTEXT ( 3 ) GLOBAL_UNCERTAINTY_ASSIGNED_CONTEXT ( ( #8043 ) ) GLOBAL_UNIT_ASSIGNED_CONTEXT ( ( #1180, #17363, #14585 ) ) REPRESENTATION_CONTEXT ( 'NONE', 'WORKASPACE' ) );
#3618=CARTESIAN_POINT ( 'NONE',  ( 10.00000000000000178, 4.769696007084728073, 1.500000000000000000 ) ) ;
#3621=AXIS2_PLACEMENT_3D ( 'NONE', #3147, #13344, #292 ) ;
#3622=ADVANCED_FACE ( 'NONE', ( #9417 ), #464, .T. ) ;
#3625=CARTESIAN_POINT ( 'NONE',  ( 10.00000000000000000, 24.46385708179996854, -9.514709542736643044 ) ) ;
#3626=CARTESIAN_POINT ( 'NONE',  ( 10.00000000000000000, 5.940243314904674499, -32.46095361140685753 ) ) ;
#3628=AXIS2_PLACEMENT_3D ( 'NONE', #15558, #8592, #9839 ) ;
#3629=ORIENTED_EDGE ( 'NONE', *, *, #8452, .T. ) ;
#3634=CARTESIAN_POINT ( 'NONE',  ( 10.00000000000000000, -27.72801475327278453, -5.086963483077506787 ) ) ;
#3644=ORIENTED_EDGE ( 'NONE', *, *, #3420, .T. ) ;
#3646=EDGE_CURVE ( 'NONE', #11016, #6635, #4447, .T. ) ;
#3652=DIRECTION ( 'NONE',  ( 0.000000000000000000, 0.000000000000000000, 1.000000000000000000 ) ) ;
#3670=EDGE_CURVE ( 'NONE', #12797, #5515, #5021, .T. ) ;
#3673=ADVANCED_FACE ( 'NONE', ( #4752 ), #4659, .T. ) ;
#3675=CARTESIAN_POINT ( 'NONE',  ( 10.00000000000000000, -3.730438010304518492, 27.94286728106391138 ) ) ;
#3686=LINE ( 'NONE', #8252, #16214 ) ;
#3694=CIRCLE ( 'NONE', #14042, 12.00000000001200462 ) ;
#3700=DIRECTION ( 'NONE',  ( -1.000000000000000000, 0.000000000000000000, 0.000000000000000000 ) ) ;
#3702=ORIENTED_EDGE ( 'NONE', *, *, #2980, .F. ) ;
#3710=DIRECTION ( 'NONE',  ( 0.000000000000000000, 0.3090169943749481729, -0.9510565162951533091 ) ) ;
#3712=CARTESIAN_POINT ( 'NONE',  ( 10.00000000000000000, 20.32630374611185786, 16.60877409751175904 ) ) ;
#3730=DIRECTION ( 'NONE',  ( -1.000000000000000000, 0.000000000000000000, 0.000000000000000000 ) ) ;
#3733=VECTOR ( 'NONE', #660, 1000.000000000000000 ) ;
#3738=DIRECTION ( 'NONE',  ( -1.000000000000000000, 0.000000000000000000, 0.000000000000000000 ) ) ;
#3747=ORIENTED_EDGE ( 'NONE', *, *, #6030, .F. ) ;
#3749=DIRECTION ( 'NONE',  ( -1.000000000000000000, -0.000000000000000000, -0.000000000000000000 ) ) ;
#3751=EDGE_LOOP ( 'NONE', ( #10528, #15735, #13331, #7986 ) ) ;
#3757=EDGE_CURVE ( 'NONE', #12242, #8620, #3855, .T. ) ;
#3758=VERTEX_POINT ( 'NONE', #3995 ) ;
#3760=ADVANCED_FACE ( 'NONE', ( #18178 ), #12558, .T. ) ;
#3762=LINE ( 'NONE', #817, #15706 ) ;
#3766=CARTESIAN_POINT ( 'NONE',  ( 10.00000000000000000, 0.000000000000000000, 0.000000000000000000 ) ) ;
#3767=EDGE_CURVE ( 'NONE', #6042, #8506, #214, .T. ) ;
#3775=ORIENTED_EDGE ( 'NONE', *, *, #15862, .T. ) ;
#3778=ADVANCED_FACE ( 'NONE', ( #2464 ), #8368, .T. ) ;
#3779=EDGE_LOOP ( 'NONE', ( #4322, #17968, #9789, #10153 ) ) ;
#3781=ADVANCED_FACE ( 'NONE', ( #10935 ), #14176, .T. ) ;
#3782=EDGE_CURVE ( 'NONE', #17821, #6186, #12372, .T. ) ;
#3789=CARTESIAN_POINT ( 'NONE',  ( 0.000000000000000000, -16.60877409751182654, 20.32630374611179391 ) ) ;
#3790=DIRECTION ( 'NONE',  ( 0.000000000000000000, 1.000000000000000000, 3.491481338843133355E-15 ) ) ;
#3791=ORIENTED_EDGE ( 'NONE', *, *, #1967, .F. ) ;
#3793=ORIENTED_EDGE ( 'NONE', *, *, #8448, .T. ) ;
#3799=LINE ( 'NONE', #3712, #12737 ) ;
#3802=AXIS2_PLACEMENT_3D ( 'NONE', #1057, #15626, #14300 ) ;
#3820=FACE_OUTER_BOUND ( 'NONE', #9248, .T. ) ;
#3821=DIRECTION ( 'NONE',  ( 0.000000000000000000, 0.000000000000000000, 1.000000000000000000 ) ) ;
#3826=AXIS2_PLACEMENT_3D ( 'NONE', #11298, #13872, #16743 ) ;
#3827=AXIS2_PLACEMENT_3D ( 'NONE', #15746, #9746, #17368 ) ;
#3838=CARTESIAN_POINT ( 'NONE',  ( 10.00000000000000000, 3.730438010304324425, 27.94286728106393980 ) ) ;
#3852=LINE ( 'NONE', #15198, #10033 ) ;
#3855=CIRCLE ( 'NONE', #12946, 12.00000000001200640 ) ;
#3859=AXIS2_PLACEMENT_3D ( 'NONE', #2297, #9446, #15344 ) ;
#3873=DIRECTION ( 'NONE',  ( 0.000000000000000000, 0.9510565162951523099, 0.3090169943749516701 ) ) ;
#3878=CARTESIAN_POINT ( 'NONE',  ( 0.000000000000000000, -25.42247726998005675, -12.18267823974779240 ) ) ;
#3895=VERTEX_POINT ( 'NONE', #14548 ) ;
#3896=EDGE_CURVE ( 'NONE', #18659, #13886, #16585, .T. ) ;
#3898=CARTESIAN_POINT ( 'NONE',  ( 10.00000000000000000, 27.72801475327274900, 5.086963483077687975 ) ) ;
#3899=ORIENTED_EDGE ( 'NONE', *, *, #15357, .F. ) ;
#3904=CARTESIAN_POINT ( 'NONE',  ( 10.00000000000000000, 12.18267823974788122, -25.42247726998001411 ) ) ;
#3908=VECTOR ( 'NONE', #3730, 1000.000000000000000 ) ;
#3909=ADVANCED_FACE ( 'NONE', ( #17498 ), #8555, .T. ) ;
#3913=EDGE_CURVE ( 'NONE', #12565, #11990, #10262, .T. ) ;
#3934=VECTOR ( 'NONE', #10500, 1000.000000000000000 ) ;
#3950=ORIENTED_EDGE ( 'NONE', *, *, #14984, .F. ) ;
#3961=VECTOR ( 'NONE', #2481, 1000.000000000000000 ) ;
#3978=CARTESIAN_POINT ( 'NONE',  ( 10.00000000000000000, -1.489278925039337453, -26.20671763660629949 ) ) ;
#3983=VECTOR ( 'NONE', #12117, 1000.000000000000000 ) ;
#3985=DIRECTION ( 'NONE',  ( 0.000000000000000000, 0.000000000000000000, 1.000000000000000000 ) ) ;
#3989=DIRECTION ( 'NONE',  ( 0.000000000000000000, 0.000000000000000000, 1.000000000000000000 ) ) ;
#3991=DIRECTION ( 'NONE',  ( 0.000000000000000000, 0.000000000000000000, 1.000000000000000000 ) ) ;
#3992=CARTESIAN_POINT ( 'NONE',  ( 0.000000000000000000, 3.730438010304324425, 27.94286728106393980 ) ) ;
#3995=CARTESIAN_POINT ( 'NONE',  ( 10.00000000000000000, 23.88582760061514421, -22.76987570971500929 ) ) ;
#4002=EDGE_CURVE ( 'NONE', #12565, #195, #14810, .T. ) ;
#4004=ORIENTED_EDGE ( 'NONE', *, *, #14408, .F. ) ;
#4008=DIRECTION ( 'NONE',  ( 0.000000000000000000, 0.000000000000000000, 1.000000000000000000 ) ) ;
#4031=ORIENTED_EDGE ( 'NONE', *, *, #7053, .F. ) ;
#4036=CARTESIAN_POINT ( 'NONE',  ( 10.00000000000000000, -5.940243314903991489, -32.46095361140698543 ) ) ;
#4038=CARTESIAN_POINT ( 'NONE',  ( 10.00000000000000000, 0.000000000000000000, 0.000000000000000000 ) ) ;
#4042=VERTEX_POINT ( 'NONE', #1682 ) ;
#4050=CARTESIAN_POINT ( 'NONE',  ( 10.00000000000000000, 20.32630374611185786, 16.60877409751175904 ) ) ;
#4054=CARTESIAN_POINT ( 'NONE',  ( 10.00000000000000000, 0.000000000000000000, 0.000000000000000000 ) ) ;
#4055=DIRECTION ( 'NONE',  ( 0.000000000000000000, 1.000000000000000000, 3.491481338843133355E-15 ) ) ;
#4059=CARTESIAN_POINT ( 'NONE',  ( 10.00000000000000000, 16.60877409751168443, 20.32630374611190405 ) ) ;
#4065=VERTEX_POINT ( 'NONE', #10441 ) ;
#4078=CARTESIAN_POINT ( 'NONE',  ( 10.00000000000000000, 0.000000000000000000, 0.000000000000000000 ) ) ;
#4087=CARTESIAN_POINT ( 'NONE',  ( 10.00000000000000000, -20.41355805489602204, -19.44239304137396118 ) ) ;
#4101=EDGE_CURVE ( 'NONE', #9667, #10550, #12969, .T. ) ;
#4103=DIRECTION ( 'NONE',  ( -1.000000000000000000, 0.000000000000000000, -0.000000000000000000 ) ) ;
#4106=CYLINDRICAL_SURFACE ( 'NONE', #13374, 12.00000000001200107 ) ;
#4124=EDGE_CURVE ( 'NONE', #6225, #15269, #15372, .T. ) ;
#4127=DIRECTION ( 'NONE',  ( 0.000000000000000000, 0.000000000000000000, 1.000000000000000000 ) ) ;
#4128=EDGE_LOOP ( 'NONE', ( #15888, #11696, #18574, #9456, #462, #10346, #9599, #11708, #5405, #18054, #3591, #5471, #3111, #15508, #7966, #15270, #82, #3329, #6344, #3119, #16119, #3254, #13926, #13969, #5747, #4373, #18369, #11733, #5891, #710, #3400, #5852, #14972, #18316, #18028, #11470, #716, #13918, #14413, #8028, #10248, #5289, #9158, #16996, #12047, #9560, #18801, #12225, #954, #13815, #2186, #10955, #18046, #5002, #14930, #16259, #12601, #14020, #17803, #11601, #10508, #3469, #4004, #2217, #11398, #14035, #18231, #2826, #15899, #3747, #2092, #15389, #15747, #9300, #5219, #16826, #259, #14356, #1419, #17388, #7042, #5597, #6019, #3245, #8321 ) ) ;
#4130=ORIENTED_EDGE ( 'NONE', *, *, #5680, .F. ) ;
#4132=CARTESIAN_POINT ( 'NONE',  ( 5.000000000000000000, -14.27431201565505425, -29.75305054077487199 ) ) ;
#4136=EDGE_CURVE ( 'NONE', #12242, #6225, #12338, .T. ) ;
#4146=VECTOR ( 'NONE', #3470, 1000.000000000000000 ) ;
#4152=CARTESIAN_POINT ( 'NONE',  ( 0.000000000000000000, 6.681932690256967788, 25.38428207620324883 ) ) ;
#4165=AXIS2_PLACEMENT_3D ( 'NONE', #15259, #8013, #14025 ) ;
#4175=AXIS2_PLACEMENT_3D ( 'NONE', #10080, #14364, #4448 ) ;
#4176=ORIENTED_EDGE ( 'NONE', *, *, #2980, .T. ) ;
#4186=DIRECTION ( 'NONE',  ( 1.000000000000000000, 0.000000000000000000, 0.000000000000000000 ) ) ;
#4188=CARTESIAN_POINT ( 'NONE',  ( 4.999999999999999112, 4.381479206523446912, -32.70783759231082399 ) ) ;
#4193=VECTOR ( 'NONE', #7476, 1000.000000000000000 ) ;
#4202=EDGE_CURVE ( 'NONE', #16450, #15559, #15696, .T. ) ;
#4203=CARTESIAN_POINT ( 'NONE',  ( 10.00000000000000000, -3.730438010304518492, 27.94286728106391138 ) ) ;
#4209=DIRECTION ( 'NONE',  ( 1.000000000000000000, 0.000000000000000000, 0.000000000000000000 ) ) ;
#4214=AXIS2_PLACEMENT_3D ( 'NONE', #18532, #17300, #5576 ) ;
#4217=CARTESIAN_POINT ( 'NONE',  ( 10.00000000000000000, 0.000000000000000000, 0.000000000000000000 ) ) ;
#4218=DIRECTION ( 'NONE',  ( 1.000000000000000000, -0.000000000000000000, -0.000000000000000000 ) ) ;
#4226=CARTESIAN_POINT ( 'NONE',  ( 10.00000000000000000, -27.94286728106395756, 15.73043801031622912 ) ) ;
#4231=CARTESIAN_POINT ( 'NONE',  ( 0.000000000000000000, -16.60877409751153522, -20.32630374611203194 ) ) ;
#4239=CIRCLE ( 'NONE', #15172, 33.00000000003299760 ) ;
#4247=CIRCLE ( 'NONE', #3628, 33.00000000003299760 ) ;
#4251=EDGE_CURVE ( 'NONE', #8328, #13117, #1302, .T. ) ;
#4252=DIRECTION ( 'NONE',  ( -1.000000000000000000, 0.000000000000000000, 0.000000000000000000 ) ) ;
#4264=CARTESIAN_POINT ( 'NONE',  ( 10.00000000000000000, 32.70783759231085952, -4.381479206523099634 ) ) ;
#4267=VERTEX_POINT ( 'NONE', #7011 ) ;
#4269=AXIS2_PLACEMENT_3D ( 'NONE', #15776, #17571, #14250 ) ;
#4272=VERTEX_POINT ( 'NONE', #17311 ) ;
#4273=CARTESIAN_POINT ( 'NONE',  ( 0.000000000000000000, 14.27431201565524788, 29.75305054077477607 ) ) ;
#4287=ORIENTED_EDGE ( 'NONE', *, *, #1104, .F. ) ;
#4290=CYLINDRICAL_SURFACE ( 'NONE', #12929, 12.00000000001200462 ) ;
#4299=CARTESIAN_POINT ( 'NONE',  ( 10.00000000000000000, 5.086963483077590276, -27.72801475327276677 ) ) ;
#4304=ORIENTED_EDGE ( 'NONE', *, *, #272, .F. ) ;
#4311=DIRECTION ( 'NONE',  ( -1.000000000000000000, -0.000000000000000000, 0.000000000000000000 ) ) ;
#4314=DIRECTION ( 'NONE',  ( -1.000000000000000000, 0.000000000000000000, 0.000000000000000000 ) ) ;
#4319=VERTEX_POINT ( 'NONE', #5777 ) ;
#4322=ORIENTED_EDGE ( 'NONE', *, *, #4470, .F. ) ;
#4324=ORIENTED_EDGE ( 'NONE', *, *, #11471, .T. ) ;
#4345=AXIS2_PLACEMENT_3D ( 'NONE', #3898, #18271, #2461 ) ;
#4346=DIRECTION ( 'NONE',  ( -1.000000000000000000, 0.000000000000000000, 0.000000000000000000 ) ) ;
#4347=CARTESIAN_POINT ( 'NONE',  ( 0.000000000000000000, 0.000000000000000000, 5.000000000000000000 ) ) ;
#4351=CARTESIAN_POINT ( 'NONE',  ( 0.000000000000000000, 24.46385708179984064, 9.514709542736980552 ) ) ;
#4358=ORIENTED_EDGE ( 'NONE', *, *, #16168, .T. ) ;
#4373=ORIENTED_EDGE ( 'NONE', *, *, #3526, .F. ) ;
#4379=CARTESIAN_POINT ( 'NONE',  ( 10.00000000000000000, -6.681932690257146312, 25.38428207620320620 ) ) ;
#4389=AXIS2_PLACEMENT_3D ( 'NONE', #18604, #8687, #10211 ) ;
#4396=LINE ( 'NONE', #17366, #10271 ) ;
#4401=EDGE_LOOP ( 'NONE', ( #2172, #17997, #14505, #6791 ) ) ;
#4407=AXIS2_PLACEMENT_3D ( 'NONE', #3295, #4622, #16061 ) ;
#4410=CARTESIAN_POINT ( 'NONE',  ( 0.000000000000000000, -27.72801475327278453, -5.086963483077506787 ) ) ;
#4423=ORIENTED_EDGE ( 'NONE', *, *, #10677, .T. ) ;
#4430=VERTEX_POINT ( 'NONE', #4231 ) ;
#4436=VERTEX_POINT ( 'NONE', #4899 ) ;
#4447=CIRCLE ( 'NONE', #15101, 12.00000000001200462 ) ;
#4448=DIRECTION ( 'NONE',  ( 0.000000000000000000, 0.000000000000000000, 1.000000000000000000 ) ) ;
#4454=AXIS2_PLACEMENT_3D ( 'NONE', #4720, #10532, #439 ) ;
#4456=EDGE_CURVE ( 'NONE', #5675, #10144, #11856, .T. ) ;
#4459=AXIS2_PLACEMENT_3D ( 'NONE', #6944, #9796, #5312 ) ;
#4466=CARTESIAN_POINT ( 'NONE',  ( 0.000000000000000000, 29.03656532225586062, -15.68049343255964878 ) ) ;
#4470=EDGE_CURVE ( 'NONE', #6348, #10144, #13576, .T. ) ;
#4475=DIRECTION ( 'NONE',  ( -1.000000000000000000, -0.000000000000000000, 0.000000000000000000 ) ) ;
#4486=VERTEX_POINT ( 'NONE', #6045 ) ;
#4498=CARTESIAN_POINT ( 'NONE',  ( 10.00000000000000000, 15.68049343256038064, -29.03656532225546627 ) ) ;
#4500=VECTOR ( 'NONE', #16574, 1000.000000000000000 ) ;
#4502=VERTEX_POINT ( 'NONE', #16238 ) ;
#4505=DIRECTION ( 'NONE',  ( 0.000000000000000000, 0.9510565162951523099, 0.3090169943749515591 ) ) ;
#4512=FACE_OUTER_BOUND ( 'NONE', #14918, .T. ) ;
#4519=CYLINDRICAL_SURFACE ( 'NONE', #264, 26.24900000002624978 ) ;
#4524=DIRECTION ( 'NONE',  ( -1.000000000000000000, -0.000000000000000000, 0.000000000000000000 ) ) ;
#4532=AXIS2_PLACEMENT_3D ( 'NONE', #778, #8208, #14010 ) ;
#4536=CARTESIAN_POINT ( 'NONE',  ( 0.000000000000000000, 26.20671763660628528, -1.489278925039611901 ) ) ;
#4538=DIRECTION ( 'NONE',  ( -1.000000000000000000, -0.000000000000000000, -0.000000000000000000 ) ) ;
#4544=VECTOR ( 'NONE', #5333, 1000.000000000000000 ) ;
#4548=CIRCLE ( 'NONE', #17627, 12.00000000001200640 ) ;
#4553=ORIENTED_EDGE ( 'NONE', *, *, #13299, .F. ) ;
#4561=DIRECTION ( 'NONE',  ( -1.000000000000000000, 0.000000000000000000, -0.000000000000000000 ) ) ;
#4565=CARTESIAN_POINT ( 'NONE',  ( 0.000000000000000000, 32.70783759231086663, 4.381479206523104963 ) ) ;
#4566=EDGE_CURVE ( 'NONE', #9120, #8129, #15709, .T. ) ;
#4567=DIRECTION ( 'NONE',  ( -1.000000000000000000, 0.000000000000000000, -0.000000000000000000 ) ) ;
#4580=ORIENTED_EDGE ( 'NONE', *, *, #13871, .F. ) ;
#4593=ORIENTED_EDGE ( 'NONE', *, *, #3280, .F. ) ;
#4598=ORIENTED_EDGE ( 'NONE', *, *, #18297, .F. ) ;
#4613=ORIENTED_EDGE ( 'NONE', *, *, #12615, .T. ) ;
#4617=CARTESIAN_POINT ( 'NONE',  ( 10.00000000000000000, 0.000000000000000000, 0.000000000000000000 ) ) ;
#4622=DIRECTION ( 'NONE',  ( -1.000000000000000000, -0.000000000000000000, 0.000000000000000000 ) ) ;
#4624=ORIENTED_EDGE ( 'NONE', *, *, #12143, .F. ) ;
#4625=DIRECTION ( 'NONE',  ( 0.000000000000000000, 0.000000000000000000, 1.000000000000000000 ) ) ;
#4626=AXIS2_PLACEMENT_3D ( 'NONE', #10086, #14735, #10172 ) ;
#4628=CYLINDRICAL_SURFACE ( 'NONE', #2378, 12.00000000001200462 ) ;
#4637=EDGE_CURVE ( 'NONE', #8129, #11016, #7191, .T. ) ;
#4655=LINE ( 'NONE', #11623, #18127 ) ;
#4658=DIRECTION ( 'NONE',  ( 0.000000000000000000, 0.000000000000000000, 1.000000000000000000 ) ) ;
#4659=CYLINDRICAL_SURFACE ( 'NONE', #5374, 12.00000000001200462 ) ;
#4671=CARTESIAN_POINT ( 'NONE',  ( 0.000000000000000000, 25.38428207620331634, -6.681932690256706664 ) ) ;
#4678=ORIENTED_EDGE ( 'NONE', *, *, #10356, .F. ) ;
#4682=ORIENTED_EDGE ( 'NONE', *, *, #1308, .T. ) ;
#4686=FACE_OUTER_BOUND ( 'NONE', #2018, .T. ) ;
#4689=CARTESIAN_POINT ( 'NONE',  ( 10.00000000000000000, -26.20671763660627462, -1.489278925039791535 ) ) ;
#4714=ORIENTED_EDGE ( 'NONE', *, *, #13299, .T. ) ;
#4720=CARTESIAN_POINT ( 'NONE',  ( -10.00000000000000000, 0.000000000000000000, 0.000000000000000000 ) ) ;
#4721=CARTESIAN_POINT ( 'NONE',  ( 0.000000000000000000, -5.086963483077402870, 27.72801475327280585 ) ) ;
#4729=DIRECTION ( 'NONE',  ( 0.000000000000000000, -6.938893903900287191E-15, 1.000000000000000000 ) ) ;
#4731=CIRCLE ( 'NONE', #10803, 12.00000000001200462 ) ;
#4733=ORIENTED_EDGE ( 'NONE', *, *, #13486, .T. ) ;
#4737=FACE_OUTER_BOUND ( 'NONE', #4401, .T. ) ;
#4744=CARTESIAN_POINT ( 'NONE',  ( 10.00000000000000000, 0.000000000000000000, 0.000000000000000000 ) ) ;
#4750=VECTOR ( 'NONE', #7871, 1000.000000000000000 ) ;
#4752=FACE_OUTER_BOUND ( 'NONE', #13962, .T. ) ;
#4760=VECTOR ( 'NONE', #1251, 1000.000000000000000 ) ;
#4774=AXIS2_PLACEMENT_3D ( 'NONE', #12462, #9790, #854 ) ;
#4786=CIRCLE ( 'NONE', #2051, 12.00000000001200462 ) ;
#4789=LINE ( 'NONE', #8799, #18571 ) ;
#4795=ORIENTED_EDGE ( 'NONE', *, *, #6534, .F. ) ;
#4803=DIRECTION ( 'NONE',  ( -1.000000000000000000, 0.000000000000000000, 0.000000000000000000 ) ) ;
#4808=ORIENTED_EDGE ( 'NONE', *, *, #2262, .T. ) ;
#4825=AXIS2_PLACEMENT_3D ( 'NONE', #2858, #8657, #14465 ) ;
#4831=VERTEX_POINT ( 'NONE', #11036 ) ;
#4835=ORIENTED_EDGE ( 'NONE', *, *, #16007, .T. ) ;
#4845=DIRECTION ( 'NONE',  ( 0.000000000000000000, -0.9510565162951565288, 0.3090169943749382919 ) ) ;
#4853=ORIENTED_EDGE ( 'NONE', *, *, #15326, .T. ) ;
#4855=LINE ( 'NONE', #16280, #7693 ) ;
#4859=ORIENTED_EDGE ( 'NONE', *, *, #17830, .F. ) ;
#4868=CYLINDRICAL_SURFACE ( 'NONE', #4532, 26.24900000002624978 ) ;
#4886=DIRECTION ( 'NONE',  ( 0.000000000000000000, 0.5877852522924742473, -0.8090169943749465631 ) ) ;
#4899=CARTESIAN_POINT ( 'NONE',  ( 10.00000000000000000, -22.07705612348849655, 14.19907017806860949 ) ) ;
#4900=AXIS2_PLACEMENT_3D ( 'NONE', #10067, #17320, #18728 ) ;
#4913=CARTESIAN_POINT ( 'NONE',  ( 10.00000000000000000, 0.000000000000000000, 0.000000000000000000 ) ) ;
#4916=CYLINDRICAL_SURFACE ( 'NONE', #4454, 33.00000000003299760 ) ;
#4931=DIRECTION ( 'NONE',  ( 0.000000000000000000, 0.5877852522924684742, 0.8090169943749507819 ) ) ;
#4936=CARTESIAN_POINT ( 'NONE',  ( 10.00000000000000000, 27.94286728106393269, 3.730438010304423013 ) ) ;
#4944=CARTESIAN_POINT ( 'NONE',  ( 0.000000000000000000, -27.72801475327278453, -5.086963483077506787 ) ) ;
#4967=CARTESIAN_POINT ( 'NONE',  ( 10.00000000000000000, -9.514709542737069370, 24.46385708179980512 ) ) ;
#4970=CARTESIAN_POINT ( 'NONE',  ( 10.00000000000000000, 27.94286728106393269, 3.730438010304423013 ) ) ;
#4971=FACE_OUTER_BOUND ( 'NONE', #7009, .T. ) ;
#4976=ADVANCED_FACE ( 'NONE', ( #15900 ), #15987, .T. ) ;
#4986=MECHANICAL_DESIGN_GEOMETRIC_PRESENTATION_REPRESENTATION('',(#1957),#2255);
#4987=EDGE_CURVE ( 'NONE', #16693, #6780, #8744, .T. ) ;
#4998=EDGE_LOOP ( 'NONE', ( #11032, #12903, #7537, #11564 ) ) ;
#5002=ORIENTED_EDGE ( 'NONE', *, *, #2486, .F. ) ;
#5013=CARTESIAN_POINT ( 'NONE',  ( 10.00000000000000000, 0.000000000000000000, 0.000000000000000000 ) ) ;
#5021=LINE ( 'NONE', #289, #5679 ) ;
#5056=CIRCLE ( 'NONE', #15717, 26.24900000002626044 ) ;
#5057=EDGE_LOOP ( 'NONE', ( #9885, #9033, #15805, #18563 ) ) ;
#5060=CYLINDRICAL_SURFACE ( 'NONE', #3859, 12.00000000001200462 ) ;
#5068=CARTESIAN_POINT ( 'NONE',  ( 10.00000000000000000, 0.000000000000000000, 0.000000000000000000 ) ) ;
#5087=CIRCLE ( 'NONE', #2663, 12.00000000001200284 ) ;
#5093=CARTESIAN_POINT ( 'NONE',  ( 10.00000000000000000, 14.27431201565524610, 29.75305054077477607 ) ) ;
#5100=CARTESIAN_POINT ( 'NONE',  ( 10.00000000000000000, 1.489278925039883239, -26.20671763660627107 ) ) ;
#5106=SURFACE_STYLE_FILL_AREA ( #1964 ) ;
#5107=EDGE_CURVE ( 'NONE', #5250, #4319, #1736, .T. ) ;
#5109=DIRECTION ( 'NONE',  ( -1.000000000000000000, 0.000000000000000000, -0.000000000000000000 ) ) ;
#5111=CIRCLE ( 'NONE', #9680, 26.24900000002624978 ) ;
#5118=DIRECTION ( 'NONE',  ( -1.000000000000000000, -0.000000000000000000, -0.000000000000000000 ) ) ;
#5129=AXIS2_PLACEMENT_3D ( 'NONE', #5544, #17437, #12877 ) ;
#5142=DIRECTION ( 'NONE',  ( 0.000000000000000000, 0.3090169943749410120, 0.9510565162951556406 ) ) ;
#5149=EDGE_CURVE ( 'NONE', #3146, #16250, #6168, .T. ) ;
#5168=CARTESIAN_POINT ( 'NONE',  ( 0.000000000000000000, 0.000000000000000000, 0.000000000000000000 ) ) ;
#5169=DIRECTION ( 'NONE',  ( 0.000000000000000000, 0.000000000000000000, 1.000000000000000000 ) ) ;
#5171=VERTEX_POINT ( 'NONE', #184 ) ;
#5183=ORIENTED_EDGE ( 'NONE', *, *, #9341, .T. ) ;
#5194=VECTOR ( 'NONE', #13525, 1000.000000000000000 ) ;
#5200=EDGE_CURVE ( 'NONE', #4436, #7904, #11487, .T. ) ;
#5204=CIRCLE ( 'NONE', #1569, 33.00000000003299760 ) ;
#5208=CARTESIAN_POINT ( 'NONE',  ( 5.000000000000000000, 15.68049343255996320, 29.03656532225569009 ) ) ;
#5216=CARTESIAN_POINT ( 'NONE',  ( 5.000000000000000000, -22.76987570971509811, -23.88582760061506249 ) ) ;
#5219=ORIENTED_EDGE ( 'NONE', *, *, #10170, .F. ) ;
#5220=ADVANCED_FACE ( 'NONE', ( #5983 ), #8746, .T. ) ;
#5226=EDGE_CURVE ( 'NONE', #18793, #4272, #2349, .T. ) ;
#5227=ORIENTED_EDGE ( 'NONE', *, *, #10187, .T. ) ;
#5250=VERTEX_POINT ( 'NONE', #17514 ) ;
#5260=LINE ( 'NONE', #10778, #16080 ) ;
#5264=DIRECTION ( 'NONE',  ( -1.000000000000000000, -0.000000000000000000, -0.000000000000000000 ) ) ;
#5265=ORIENTED_EDGE ( 'NONE', *, *, #11324, .T. ) ;
#5269=CARTESIAN_POINT ( 'NONE',  ( 10.00000000000000000, 0.000000000000000000, 0.000000000000000000 ) ) ;
#5273=ADVANCED_FACE ( 'NONE', ( #2855 ), #11265, .T. ) ;
#5289=ORIENTED_EDGE ( 'NONE', *, *, #3646, .F. ) ;
#5291=DIRECTION ( 'NONE',  ( 0.000000000000000000, 0.000000000000000000, -1.000000000000000000 ) ) ;
#5299=VERTEX_POINT ( 'NONE', #16464 ) ;
#5307=ORIENTED_EDGE ( 'NONE', *, *, #14012, .T. ) ;
#5308=DIRECTION ( 'NONE',  ( -1.000000000000000000, -0.000000000000000000, 0.000000000000000000 ) ) ;
#5312=DIRECTION ( 'NONE',  ( 0.000000000000000000, 0.000000000000000000, 1.000000000000000000 ) ) ;
#5318=AXIS2_PLACEMENT_3D ( 'NONE', #15031, #3700, #18354 ) ;
#5321=VERTEX_POINT ( 'NONE', #279 ) ;
#5325=CARTESIAN_POINT ( 'NONE',  ( 0.000000000000000000, 0.000000000000000000, 0.000000000000000000 ) ) ;
#5330=CIRCLE ( 'NONE', #9281, 12.00000000001200817 ) ;
#5332=ORIENTED_EDGE ( 'NONE', *, *, #5959, .F. ) ;
#5333=DIRECTION ( 'NONE',  ( -1.000000000000000000, 0.000000000000000000, -0.000000000000000000 ) ) ;
#5336=CARTESIAN_POINT ( 'NONE',  ( 10.00000000000000000, 13.40641754777700534, -24.79895094899245933 ) ) ;
#5337=CARTESIAN_POINT ( 'NONE',  ( 0.000000000000000000, 13.40641754777665717, 24.79895094899264052 ) ) ;
#5341=VECTOR ( 'NONE', #8711, 1000.000000000000000 ) ;
#5347=DIRECTION ( 'NONE',  ( 0.000000000000000000, -0.5877852522924801315, 0.8090169943749422332 ) ) ;
#5351=CARTESIAN_POINT ( 'NONE',  ( 0.000000000000000000, 0.000000000000000000, 0.000000000000000000 ) ) ;
#5358=DIRECTION ( 'NONE',  ( -1.000000000000000000, -0.000000000000000000, -0.000000000000000000 ) ) ;
#5366=EDGE_LOOP ( 'NONE', ( #5958, #10697, #12416, #12600, #17716, #8819 ) ) ;
#5367=CIRCLE ( 'NONE', #3236, 26.24900000002624978 ) ;
#5373=AXIS2_PLACEMENT_3D ( 'NONE', #1420, #13048, #7 ) ;
#5374=AXIS2_PLACEMENT_3D ( 'NONE', #3342, #6180, #9137 ) ;
#5375=DIRECTION ( 'NONE',  ( -1.000000000000000000, 0.000000000000000000, -0.000000000000000000 ) ) ;
#5378=VECTOR ( 'NONE', #5567, 1000.000000000000000 ) ;
#5383=ORIENTED_EDGE ( 'NONE', *, *, #10220, .T. ) ;
#5384=ADVANCED_FACE ( 'NONE', ( #1694 ), #7508, .T. ) ;
#5390=AXIS2_PLACEMENT_3D ( 'NONE', #1076, #10368, #16089 ) ;
#5396=EDGE_LOOP ( 'NONE', ( #18537, #8573, #748, #14153 ) ) ;
#5402=EDGE_CURVE ( 'NONE', #9858, #3146, #1147, .T. ) ;
#5405=ORIENTED_EDGE ( 'NONE', *, *, #5768, .F. ) ;
#5412=CIRCLE ( 'NONE', #12091, 26.24900000002624978 ) ;
#5413=DIRECTION ( 'NONE',  ( 0.000000000000000000, -0.9510565162951502005, -0.3090169943749581649 ) ) ;
#5433=AXIS2_PLACEMENT_3D ( 'NONE', #9473, #821, #921 ) ;
#5436=AXIS2_PLACEMENT_3D ( 'NONE', #16796, #6414, #8128 ) ;
#5441=DIRECTION ( 'NONE',  ( -1.000000000000000000, -0.000000000000000000, -0.000000000000000000 ) ) ;
#5443=DIRECTION ( 'NONE',  ( 1.000000000000000000, 0.000000000000000000, -0.000000000000000000 ) ) ;
#5444=CARTESIAN_POINT ( 'NONE',  ( 0.000000000000000000, -23.88582760061464683, -22.76987570971553865 ) ) ;
#5449=FACE_OUTER_BOUND ( 'NONE', #13440, .T. ) ;
#5460=LINE ( 'NONE', #11259, #17243 ) ;
#5464=EDGE_CURVE ( 'NONE', #7978, #6225, #10572, .T. ) ;
#5471=ORIENTED_EDGE ( 'NONE', *, *, #16766, .F. ) ;
#5473=ADVANCED_FACE ( 'NONE', ( #5509 ), #12644, .T. ) ;
#5479=CARTESIAN_POINT ( 'NONE',  ( 10.00000000000000000, 15.68049343255996320, 29.03656532225568654 ) ) ;
#5486=EDGE_CURVE ( 'NONE', #6276, #2833, #16967, .T. ) ;
#5489=ORIENTED_EDGE ( 'NONE', *, *, #16912, .T. ) ;
#5498=DIRECTION ( 'NONE',  ( -1.000000000000000000, 0.000000000000000000, -0.000000000000000000 ) ) ;
#5507=CARTESIAN_POINT ( 'NONE',  ( 10.00000000000000000, 0.000000000000000000, 0.000000000000000000 ) ) ;
#5509=FACE_OUTER_BOUND ( 'NONE', #9503, .T. ) ;
#5512=VERTEX_POINT ( 'NONE', #947 ) ;
#5515=VERTEX_POINT ( 'NONE', #16938 ) ;
#5517=DIRECTION ( 'NONE',  ( 0.000000000000000000, 0.8090169943749487835, -0.5877852522924713607 ) ) ;
#5525=EDGE_CURVE ( 'NONE', #13562, #13630, #8149, .T. ) ;
#5533=EDGE_CURVE ( 'NONE', #13213, #11810, #9968, .T. ) ;
#5539=ORIENTED_EDGE ( 'NONE', *, *, #3757, .T. ) ;
#5541=CARTESIAN_POINT ( 'NONE',  ( 10.00000000000000000, -4.381479206523214209, 32.70783759231085241 ) ) ;
#5544=CARTESIAN_POINT ( 'NONE',  ( 0.000000000000000000, 0.000000000000000000, 0.000000000000000000 ) ) ;
#5554=CARTESIAN_POINT ( 'NONE',  ( 0.000000000000000000, 9.514709542736897063, 24.46385708179987262 ) ) ;
#5557=DIRECTION ( 'NONE',  ( 1.000000000000000000, -0.000000000000000000, -0.000000000000000000 ) ) ;
#5567=DIRECTION ( 'NONE',  ( -1.000000000000000000, 0.000000000000000000, -0.000000000000000000 ) ) ;
#5576=DIRECTION ( 'NONE',  ( 0.000000000000000000, 0.3090169943749481174, -0.9510565162951533091 ) ) ;
#5579=CARTESIAN_POINT ( 'NONE',  ( 10.00000000000000000, -23.88582760061497368, 22.76987570971519048 ) ) ;
#5586=EDGE_CURVE ( 'NONE', #16250, #14912, #9345, .T. ) ;
#5595=CARTESIAN_POINT ( 'NONE',  ( 0.000000000000000000, 25.42247726998032320, -12.18267823974723640 ) ) ;
#5597=ORIENTED_EDGE ( 'NONE', *, *, #12616, .F. ) ;
#5598=CARTESIAN_POINT ( 'NONE',  ( 10.00000000000000000, 0.000000000000000000, 0.000000000000000000 ) ) ;
#5613=CARTESIAN_POINT ( 'NONE',  ( 10.00000000000000000, -16.60877409751153522, -20.32630374611203194 ) ) ;
#5630=VERTEX_POINT ( 'NONE', #5956 ) ;
#5645=ORIENTED_EDGE ( 'NONE', *, *, #4002, .T. ) ;
#5657=VECTOR ( 'NONE', #3074, 1000.000000000000000 ) ;
#5658=EDGE_CURVE ( 'NONE', #9105, #10779, #3588, .T. ) ;
#5664=LINE ( 'NONE', #7003, #7950 ) ;
#5672=DIRECTION ( 'NONE',  ( 0.000000000000000000, 0.000000000000000000, -1.000000000000000000 ) ) ;
#5673=FACE_OUTER_BOUND ( 'NONE', #15678, .T. ) ;
#5675=VERTEX_POINT ( 'NONE', #7392 ) ;
#5679=VECTOR ( 'NONE', #13620, 1000.000000000000000 ) ;
#5680=EDGE_CURVE ( 'NONE', #10144, #18793, #16664, .T. ) ;
#5683=CIRCLE ( 'NONE', #7803, 26.24900000002625333 ) ;
#5695=CIRCLE ( 'NONE', #11148, 33.00000000003299760 ) ;
#5699=CIRCLE ( 'NONE', #17551, 33.00000000003299760 ) ;
#5707=DIRECTION ( 'NONE',  ( 1.000000000000000000, -0.000000000000000000, 0.000000000000000000 ) ) ;
#5709=LINE ( 'NONE', #8646, #15877 ) ;
#5716=CARTESIAN_POINT ( 'NONE',  ( 0.000000000000000000, -5.940243314903989713, -32.46095361140699254 ) ) ;
#5718=DIRECTION ( 'NONE',  ( -1.000000000000000000, 0.000000000000000000, 0.000000000000000000 ) ) ;
#5727=CARTESIAN_POINT ( 'NONE',  ( 10.00000000000000000, 0.000000000000000000, 0.000000000000000000 ) ) ;
#5734=ORIENTED_EDGE ( 'NONE', *, *, #4987, .F. ) ;
#5741=DIRECTION ( 'NONE',  ( -1.000000000000000000, -0.000000000000000000, 0.000000000000000000 ) ) ;
#5747=ORIENTED_EDGE ( 'NONE', *, *, #16977, .F. ) ;
#5751=CARTESIAN_POINT ( 'NONE',  ( 10.00000000000000000, 20.32630374611208879, -16.60877409751146416 ) ) ;
#5754=VERTEX_POINT ( 'NONE', #10624 ) ;
#5762=EDGE_CURVE ( 'NONE', #13152, #11197, #12398, .T. ) ;
#5764=VECTOR ( 'NONE', #8868, 1000.000000000000000 ) ;
#5768=EDGE_CURVE ( 'NONE', #9230, #16428, #17896, .T. ) ;
#5777=CARTESIAN_POINT ( 'NONE',  ( 10.00000000000000000, -24.46385708179990459, 9.514709542736804693 ) ) ;
#5781=CARTESIAN_POINT ( 'NONE',  ( 0.000000000000000000, 0.000000000000000000, 26.24900000002624978 ) ) ;
#5782=CARTESIAN_POINT ( 'NONE',  ( 10.00000000000000000, 27.72801475327282361, 6.913036516934699449 ) ) ;
#5783=VERTEX_POINT ( 'NONE', #7868 ) ;
#5784=LINE ( 'NONE', #9782, #636 ) ;
#5789=ORIENTED_EDGE ( 'NONE', *, *, #16340, .T. ) ;
#5793=CARTESIAN_POINT ( 'NONE',  ( 10.00000000000000000, -5.940243314904447125, 32.46095361140690727 ) ) ;
#5818=DIRECTION ( 'NONE',  ( -1.000000000000000000, -0.000000000000000000, -0.000000000000000000 ) ) ;
#5823=CARTESIAN_POINT ( 'NONE',  ( 0.000000000000000000, -27.94286728106390072, -3.730438010304629515 ) ) ;
#5826=FACE_OUTER_BOUND ( 'NONE', #13608, .T. ) ;
#5831=VERTEX_POINT ( 'NONE', #17766 ) ;
#5836=ORIENTED_EDGE ( 'NONE', *, *, #8067, .F. ) ;
#5838=ADVANCED_FACE ( 'NONE', ( #16249, #15112 ), #3487, .F. ) ;
#5843=DIRECTION ( 'NONE',  ( -1.000000000000000000, 0.000000000000000000, -0.000000000000000000 ) ) ;
#5847=LINE ( 'NONE', #2617, #11519 ) ;
#5852=ORIENTED_EDGE ( 'NONE', *, *, #6643, .F. ) ;
#5860=ADVANCED_FACE ( 'NONE', ( #16349 ), #4628, .T. ) ;
#5862=EDGE_CURVE ( 'NONE', #18364, #10019, #5111, .T. ) ;
#5869=DIRECTION ( 'NONE',  ( 1.000000000000000000, 0.000000000000000000, 0.000000000000000000 ) ) ;
#5880=ORIENTED_EDGE ( 'NONE', *, *, #3896, .F. ) ;
#5887=EDGE_CURVE ( 'NONE', #18040, #10550, #16731, .T. ) ;
#5891=ORIENTED_EDGE ( 'NONE', *, *, #10405, .F. ) ;
#5897=FACE_OUTER_BOUND ( 'NONE', #13495, .T. ) ;
#5902=CYLINDRICAL_SURFACE ( 'NONE', #1119, 12.00000000001200462 ) ;
#5903=ORIENTED_EDGE ( 'NONE', *, *, #1687, .T. ) ;
#5904=CARTESIAN_POINT ( 'NONE',  ( 0.000000000000000000, 0.000000000000000000, 0.000000000000000000 ) ) ;
#5905=CARTESIAN_POINT ( 'NONE',  ( 10.00000000000000000, 0.000000000000000000, 0.000000000000000000 ) ) ;
#5911=CARTESIAN_POINT ( 'NONE',  ( 0.000000000000000000, 24.46385708179996854, -9.514709542736643044 ) ) ;
#5917=ORIENTED_EDGE ( 'NONE', *, *, #13158, .T. ) ;
#5919=DIRECTION ( 'NONE',  ( -1.000000000000000000, 0.000000000000000000, 0.000000000000000000 ) ) ;
#5928=DIRECTION ( 'NONE',  ( -1.000000000000000000, 0.000000000000000000, -0.000000000000000000 ) ) ;
#5941=DIRECTION ( 'NONE',  ( 0.000000000000000000, -6.982962677686266711E-15, 1.000000000000000000 ) ) ;
#5942=DIRECTION ( 'NONE',  ( 0.000000000000000000, 0.000000000000000000, 1.000000000000000000 ) ) ;
#5956=CARTESIAN_POINT ( 'NONE',  ( 10.00000000000000000, 14.19907017806868588, 22.07705612348844326 ) ) ;
#5958=ORIENTED_EDGE ( 'NONE', *, *, #1863, .F. ) ;
#5959=EDGE_CURVE ( 'NONE', #17584, #17410, #8471, .T. ) ;
#5969=CYLINDRICAL_SURFACE ( 'NONE', #14565, 26.24900000002624978 ) ;
#5983=FACE_OUTER_BOUND ( 'NONE', #17709, .T. ) ;
#5997=CIRCLE ( 'NONE', #545, 12.00000000001200284 ) ;
#5998=AXIS2_PLACEMENT_3D ( 'NONE', #11012, #5118, #13786 ) ;
#6002=AXIS2_PLACEMENT_3D ( 'NONE', #6263, #17891, #4845 ) ;
#6007=CARTESIAN_POINT ( 'NONE',  ( 10.00000000000000000, 0.000000000000000000, 0.000000000000000000 ) ) ;
#6014=EDGE_CURVE ( 'NONE', #15251, #6022, #15666, .T. ) ;
#6019=ORIENTED_EDGE ( 'NONE', *, *, #10677, .F. ) ;
#6022=VERTEX_POINT ( 'NONE', #4152 ) ;
#6023=AXIS2_PLACEMENT_3D ( 'NONE', #12980, #5741, #7253 ) ;
#6030=EDGE_CURVE ( 'NONE', #6186, #12797, #3296, .T. ) ;
#6031=CYLINDRICAL_SURFACE ( 'NONE', #13906, 12.00000000001200107 ) ;
#6036=ORIENTED_EDGE ( 'NONE', *, *, #270, .F. ) ;
#6042=VERTEX_POINT ( 'NONE', #4059 ) ;
#6045=CARTESIAN_POINT ( 'NONE',  ( 0.000000000000000000, 4.381479206523448688, -32.70783759231082399 ) ) ;
#6057=EDGE_CURVE ( 'NONE', #4502, #16169, #10283, .T. ) ;
#6064=ORIENTED_EDGE ( 'NONE', *, *, #8679, .F. ) ;
#6072=EDGE_CURVE ( 'NONE', #7904, #4042, #10230, .T. ) ;
#6074=AXIS2_PLACEMENT_3D ( 'NONE', #15692, #17046, #3989 ) ;
#6083=EDGE_CURVE ( 'NONE', #17080, #195, #5847, .T. ) ;
#6091=DIRECTION ( 'NONE',  ( -1.000000000000000000, -0.000000000000000000, -0.000000000000000000 ) ) ;
#6093=EDGE_CURVE ( 'NONE', #18364, #16450, #7179, .T. ) ;
#6101=ORIENTED_EDGE ( 'NONE', *, *, #2162, .F. ) ;
#6102=CYLINDRICAL_SURFACE ( 'NONE', #13961, 26.24900000002624978 ) ;
#6108=DIRECTION ( 'NONE',  ( -1.000000000000000000, 0.000000000000000000, 0.000000000000000000 ) ) ;
#6114=EDGE_CURVE ( 'NONE', #5754, #17080, #17014, .T. ) ;
#6117=CIRCLE ( 'NONE', #11894, 12.00000000001200284 ) ;
#6125=CYLINDRICAL_SURFACE ( 'NONE', #530, 12.00000000001200462 ) ;
#6128=CARTESIAN_POINT ( 'NONE',  ( 10.00000000000000000, 24.46385708179984064, 9.514709542736980552 ) ) ;
#6133=ORIENTED_EDGE ( 'NONE', *, *, #8375, .T. ) ;
#6139=ORIENTED_EDGE ( 'NONE', *, *, #4101, .T. ) ;
#6147=VECTOR ( 'NONE', #15625, 1000.000000000000000 ) ;
#6148=ORIENTED_EDGE ( 'NONE', *, *, #13257, .F. ) ;
#6151=EDGE_LOOP ( 'NONE', ( #16624, #4682, #12184, #4714 ) ) ;
#6154=ORIENTED_EDGE ( 'NONE', *, *, #2162, .T. ) ;
#6158=ORIENTED_EDGE ( 'NONE', *, *, #13486, .F. ) ;
#6168=LINE ( 'NONE', #11972, #1448 ) ;
#6172=CARTESIAN_POINT ( 'NONE',  ( 10.00000000000000000, 12.18267823974751352, 25.42247726998019530 ) ) ;
#6180=DIRECTION ( 'NONE',  ( -1.000000000000000000, 0.000000000000000000, 0.000000000000000000 ) ) ;
#6182=DIRECTION ( 'NONE',  ( -1.000000000000000000, 0.000000000000000000, -0.000000000000000000 ) ) ;
#6186=VERTEX_POINT ( 'NONE', #12126 ) ;
#6187=LINE ( 'NONE', #5208, #5194 ) ;
#6189=CARTESIAN_POINT ( 'NONE',  ( 10.00000000000000000, 0.000000000000000000, 0.000000000000000000 ) ) ;
#6192=ADVANCED_FACE ( 'NONE', ( #13472 ), #4519, .T. ) ;
#6216=CYLINDRICAL_SURFACE ( 'NONE', #18473, 26.24900000002624978 ) ;
#6225=VERTEX_POINT ( 'NONE', #7647 ) ;
#6241=VERTEX_POINT ( 'NONE', #13186 ) ;
#6242=DIRECTION ( 'NONE',  ( 0.000000000000000000, 0.000000000000000000, 1.000000000000000000 ) ) ;
#6244=ORIENTED_EDGE ( 'NONE', *, *, #8492, .T. ) ;
#6248=ORIENTED_EDGE ( 'NONE', *, *, #6014, .T. ) ;
#6251=VERTEX_POINT ( 'NONE', #8972 ) ;
#6255=CARTESIAN_POINT ( 'NONE',  ( 0.000000000000000000, -15.68049343255974826, -29.03656532225581088 ) ) ;
#6260=ADVANCED_BREP_SHAPE_REPRESENTATION ( '', ( #15847, #8017 ), #11074 ) ;
#6263=CARTESIAN_POINT ( 'NONE',  ( 0.000000000000000000, 0.000000000000000000, 0.000000000000000000 ) ) ;
#6267=EDGE_CURVE ( 'NONE', #6186, #14980, #13382, .T. ) ;
#6269=CARTESIAN_POINT ( 'NONE',  ( 0.000000000000000000, 0.000000000000000000, 0.000000000000000000 ) ) ;
#6274=CARTESIAN_POINT ( 'NONE',  ( 10.00000000000000000, 5.086963483077203918, 27.72801475327284138 ) ) ;
#6276=VERTEX_POINT ( 'NONE', #16321 ) ;
#6279=ADVANCED_FACE ( 'NONE', ( #6704 ), #6792, .T. ) ;
#6285=ORIENTED_EDGE ( 'NONE', *, *, #2489, .T. ) ;
#6286=FACE_OUTER_BOUND ( 'NONE', #540, .T. ) ;
#6295=DIRECTION ( 'NONE',  ( -1.000000000000000000, 0.000000000000000000, 0.000000000000000000 ) ) ;
#6310=VECTOR ( 'NONE', #12430, 1000.000000000000000 ) ;
#6316=CARTESIAN_POINT ( 'NONE',  ( 5.000000000000000000, -29.75305054077482936, 14.27431201565513774 ) ) ;
#6333=CIRCLE ( 'NONE', #5433, 12.00000000001200462 ) ;
#6336=ADVANCED_FACE ( 'NONE', ( #18120 ), #2037, .T. ) ;
#6341=AXIS2_PLACEMENT_3D ( 'NONE', #633, #17589, #3206 ) ;
#6344=ORIENTED_EDGE ( 'NONE', *, *, #16340, .F. ) ;
#6348=VERTEX_POINT ( 'NONE', #2416 ) ;
#6353=DIRECTION ( 'NONE',  ( 1.000000000000000000, 0.000000000000000000, 0.000000000000000000 ) ) ;
#6355=ORIENTED_EDGE ( 'NONE', *, *, #6643, .T. ) ;
#6357=ORIENTED_EDGE ( 'NONE', *, *, #6894, .T. ) ;
#6360=VECTOR ( 'NONE', #11968, 1000.000000000000000 ) ;
#6364=ADVANCED_FACE ( 'NONE', ( #608 ), #702, .T. ) ;
#6371=ORIENTED_EDGE ( 'NONE', *, *, #4637, .T. ) ;
#6384=EDGE_CURVE ( 'NONE', #9892, #3169, #5260, .T. ) ;
#6401=ORIENTED_EDGE ( 'NONE', *, *, #9226, .T. ) ;
#6408=CARTESIAN_POINT ( 'NONE',  ( 10.00000000000000000, 0.000000000000000000, 0.000000000000000000 ) ) ;
#6409=CARTESIAN_POINT ( 'NONE',  ( 10.00000000000000000, -15.68049343256016570, 29.03656532225557996 ) ) ;
#6411=DIRECTION ( 'NONE',  ( -1.000000000000000000, 0.000000000000000000, 0.000000000000000000 ) ) ;
#6414=DIRECTION ( 'NONE',  ( -1.000000000000000000, 0.000000000000000000, 0.000000000000000000 ) ) ;
#6418=CARTESIAN_POINT ( 'NONE',  ( 10.00000000000000000, 0.000000000000000000, 0.000000000000000000 ) ) ;
#6419=VERTEX_POINT ( 'NONE', #7931 ) ;
#6437=EDGE_CURVE ( 'NONE', #7035, #12068, #10973, .T. ) ;
#6441=LINE ( 'NONE', #16914, #1712 ) ;
#6450=EDGE_CURVE ( 'NONE', #514, #10074, #10600, .T. ) ;
#6452=DIRECTION ( 'NONE',  ( 0.000000000000000000, 0.000000000000000000, 1.000000000000000000 ) ) ;
#6457=CARTESIAN_POINT ( 'NONE',  ( 10.00000000000000000, -14.27431201565546104, 29.75305054077466949 ) ) ;
#6459=ORIENTED_EDGE ( 'NONE', *, *, #10636, .F. ) ;
#6462=DIRECTION ( 'NONE',  ( -1.000000000000000000, 0.000000000000000000, 0.000000000000000000 ) ) ;
#6465=ORIENTED_EDGE ( 'NONE', *, *, #6596, .F. ) ;
#6470=AXIS2_PLACEMENT_3D ( 'NONE', #12215, #3371, #18024 ) ;
#6473=EDGE_CURVE ( 'NONE', #364, #15019, #7278, .T. ) ;
#6475=CIRCLE ( 'NONE', #17732, 33.00000000003299760 ) ;
#6480=DIRECTION ( 'NONE',  ( 0.000000000000000000, 0.000000000000000000, -1.000000000000000000 ) ) ;
#6487=EDGE_LOOP ( 'NONE', ( #437, #10403, #3950, #11404 ) ) ;
#6491=ORIENTED_EDGE ( 'NONE', *, *, #15039, .T. ) ;
#6493=ORIENTED_EDGE ( 'NONE', *, *, #2311, .F. ) ;
#6494=DIRECTION ( 'NONE',  ( -1.000000000000000000, 0.000000000000000000, 0.000000000000000000 ) ) ;
#6501=DIRECTION ( 'NONE',  ( -1.000000000000000000, -0.000000000000000000, 0.000000000000000000 ) ) ;
#6528=ORIENTED_EDGE ( 'NONE', *, *, #8550, .T. ) ;
#6529=ORIENTED_EDGE ( 'NONE', *, *, #6014, .F. ) ;
#6534=EDGE_CURVE ( 'NONE', #12930, #353, #4247, .T. ) ;
#6536=DIRECTION ( 'NONE',  ( 1.000000000000000000, 0.000000000000000000, 0.000000000000000000 ) ) ;
#6546=DIRECTION ( 'NONE',  ( 0.000000000000000000, 0.000000000000000000, 1.000000000000000000 ) ) ;
#6547=ORIENTED_EDGE ( 'NONE', *, *, #3670, .F. ) ;
#6552=AXIS2_PLACEMENT_3D ( 'NONE', #7313, #4186, #8640 ) ;
#6559=DIRECTION ( 'NONE',  ( -1.000000000000000000, 0.000000000000000000, -0.000000000000000000 ) ) ;
#6566=VECTOR ( 'NONE', #16425, 1000.000000000000000 ) ;
#6568=EDGE_CURVE ( 'NONE', #11810, #13117, #14880, .T. ) ;
#6569=CIRCLE ( 'NONE', #14181, 12.00000000001200462 ) ;
#6574=VECTOR ( 'NONE', #103, 1000.000000000000000 ) ;
#6583=VERTEX_POINT ( 'NONE', #1632 ) ;
#6596=EDGE_CURVE ( 'NONE', #13370, #8889, #13452, .T. ) ;
#6614=DIRECTION ( 'NONE',  ( -1.000000000000000000, 0.000000000000000000, 0.000000000000000000 ) ) ;
#6635=VERTEX_POINT ( 'NONE', #1548 ) ;
#6638=DIRECTION ( 'NONE',  ( 0.000000000000000000, -0.9510565162951565288, 0.3090169943749384029 ) ) ;
#6643=EDGE_CURVE ( 'NONE', #9892, #6992, #11836, .T. ) ;
#6649=ORIENTED_EDGE ( 'NONE', *, *, #15041, .T. ) ;
#6682=EDGE_CURVE ( 'NONE', #5250, #7010, #7630, .T. ) ;
#6684=DIRECTION ( 'NONE',  ( 0.000000000000000000, 0.000000000000000000, -1.000000000000000000 ) ) ;
#6690=ORIENTED_EDGE ( 'NONE', *, *, #341, .T. ) ;
#6696=AXIS2_PLACEMENT_3D ( 'NONE', #2529, #15295, #8050 ) ;
#6704=FACE_OUTER_BOUND ( 'NONE', #3390, .T. ) ;
#6708=DIRECTION ( 'NONE',  ( 0.000000000000000000, 0.000000000000000000, 1.000000000000000000 ) ) ;
#6715=AXIS2_PLACEMENT_3D ( 'NONE', #16699, #9349, #17931 ) ;
#6716=ADVANCED_FACE ( 'NONE', ( #10952 ), #4868, .T. ) ;
#6726=DIRECTION ( 'NONE',  ( -1.000000000000000000, 0.000000000000000000, 0.000000000000000000 ) ) ;
#6741=DIRECTION ( 'NONE',  ( -1.000000000000000000, -0.000000000000000000, -0.000000000000000000 ) ) ;
#6747=DIRECTION ( 'NONE',  ( 0.000000000000000000, -6.938893903900287191E-15, 1.000000000000000000 ) ) ;
#6756=EDGE_LOOP ( 'NONE', ( #4733, #11762, #2296, #16852 ) ) ;
#6770=DIRECTION ( 'NONE',  ( 0.000000000000000000, 0.000000000000000000, 1.000000000000000000 ) ) ;
#6780=VERTEX_POINT ( 'NONE', #2006 ) ;
#6791=ORIENTED_EDGE ( 'NONE', *, *, #16460, .T. ) ;
#6792=CYLINDRICAL_SURFACE ( 'NONE', #10296, 33.00000000003299760 ) ;
#6796=FACE_OUTER_BOUND ( 'NONE', #14226, .T. ) ;
#6801=ORIENTED_EDGE ( 'NONE', *, *, #4456, .F. ) ;
#6803=EDGE_CURVE ( 'NONE', #17453, #4430, #17329, .T. ) ;
#6810=ORIENTED_EDGE ( 'NONE', *, *, #754, .F. ) ;
#6811=EDGE_CURVE ( 'NONE', #14782, #1295, #10922, .T. ) ;
#6828=DIRECTION ( 'NONE',  ( 0.000000000000000000, -0.3090169943749549453, 0.9510565162951511997 ) ) ;
#6830=ORIENTED_EDGE ( 'NONE', *, *, #12564, .F. ) ;
#6834=DIRECTION ( 'NONE',  ( 1.000000000000000000, 0.000000000000000000, -0.000000000000000000 ) ) ;
#6836=ORIENTED_EDGE ( 'NONE', *, *, #6596, .T. ) ;
#6838=DIRECTION ( 'NONE',  ( -1.000000000000000000, -0.000000000000000000, 0.000000000000000000 ) ) ;
#6839=VERTEX_POINT ( 'NONE', #8662 ) ;
#6840=LINE ( 'NONE', #17143, #2418 ) ;
#6844=AXIS2_PLACEMENT_3D ( 'NONE', #15133, #18169, #1975 ) ;
#6845=EDGE_CURVE ( 'NONE', #1295, #7035, #599, .T. ) ;
#6853=VERTEX_POINT ( 'NONE', #5751 ) ;
#6855=DIRECTION ( 'NONE',  ( 0.000000000000000000, -0.5877852522924802425, 0.8090169943749422332 ) ) ;
#6857=ORIENTED_EDGE ( 'NONE', *, *, #2302, .T. ) ;
#6862=CARTESIAN_POINT ( 'NONE',  ( 10.00000000000000000, 29.03656532225563680, 15.68049343256006800 ) ) ;
#6868=AXIS2_PLACEMENT_3D ( 'NONE', #17294, #10133, #8428 ) ;
#6869=AXIS2_PLACEMENT_3D ( 'NONE', #1455, #6108, #16118 ) ;
#6870=ORIENTED_EDGE ( 'NONE', *, *, #10960, .T. ) ;
#6873=DIRECTION ( 'NONE',  ( -1.000000000000000000, -0.000000000000000000, -0.000000000000000000 ) ) ;
#6875=DIRECTION ( 'NONE',  ( -1.000000000000000000, -0.000000000000000000, -0.000000000000000000 ) ) ;
#6881=DIRECTION ( 'NONE',  ( -1.000000000000000000, 0.000000000000000000, 0.000000000000000000 ) ) ;
#6884=AXIS2_PLACEMENT_3D ( 'NONE', #3558, #9538, #792 ) ;
#6894=EDGE_CURVE ( 'NONE', #34, #12340, #17253, .T. ) ;
#6895=ORIENTED_EDGE ( 'NONE', *, *, #2704, .F. ) ;
#6898=DIRECTION ( 'NONE',  ( 0.000000000000000000, 0.000000000000000000, 1.000000000000000000 ) ) ;
#6913=EDGE_CURVE ( 'NONE', #24, #8001, #14302, .T. ) ;
#6919=CYLINDRICAL_SURFACE ( 'NONE', #7294, 33.00000000003299760 ) ;
#6930=ADVANCED_FACE ( 'NONE', ( #5449 ), #4106, .T. ) ;
#6940=DIRECTION ( 'NONE',  ( 0.000000000000000000, 0.000000000000000000, 1.000000000000000000 ) ) ;
#6943=ORIENTED_EDGE ( 'NONE', *, *, #11923, .T. ) ;
#6944=CARTESIAN_POINT ( 'NONE',  ( 10.00000000000000000, 13.40641754777700534, -24.79895094899245933 ) ) ;
#6946=CYLINDRICAL_SURFACE ( 'NONE', #10017, 12.00000000001200462 ) ;
#6969=LINE ( 'NONE', #972, #4146 ) ;
#6977=DIRECTION ( 'NONE',  ( -1.000000000000000000, 0.000000000000000000, -0.000000000000000000 ) ) ;
#6983=CIRCLE ( 'NONE', #17626, 12.00000000001200462 ) ;
#6987=CARTESIAN_POINT ( 'NONE',  ( 0.000000000000000000, 0.000000000000000000, 0.000000000000000000 ) ) ;
#6992=VERTEX_POINT ( 'NONE', #14573 ) ;
#6999=AXIS2_PLACEMENT_3D ( 'NONE', #322, #5843, #11930 ) ;
#7002=CARTESIAN_POINT ( 'NONE',  ( 0.000000000000000000, 0.000000000000000000, 0.000000000000000000 ) ) ;
#7003=CARTESIAN_POINT ( 'NONE',  ( 10.00000000000000000, -14.19907017806883864, 22.07705612348834734 ) ) ;
#7005=ORIENTED_EDGE ( 'NONE', *, *, #1104, .T. ) ;
#7009=EDGE_LOOP ( 'NONE', ( #1266, #2906, #8230, #1013 ) ) ;
#7010=VERTEX_POINT ( 'NONE', #17434 ) ;
#7011=CARTESIAN_POINT ( 'NONE',  ( 0.000000000000000000, 20.32630374611185786, 16.60877409751175904 ) ) ;
#7022=VERTEX_POINT ( 'NONE', #15999 ) ;
#7029=ADVANCED_FACE ( 'NONE', ( #13339 ), #11714, .T. ) ;
#7035=VERTEX_POINT ( 'NONE', #4565 ) ;
#7042=ORIENTED_EDGE ( 'NONE', *, *, #10843, .F. ) ;
#7045=CARTESIAN_POINT ( 'NONE',  ( 10.00000000000000000, 22.76987570971561325, -23.88582760061456511 ) ) ;
#7048=CYLINDRICAL_SURFACE ( 'NONE', #16396, 12.00000000001200817 ) ;
#7053=EDGE_CURVE ( 'NONE', #13562, #6419, #6983, .T. ) ;
#7054=DIRECTION ( 'NONE',  ( 0.000000000000000000, 0.000000000000000000, 1.000000000000000000 ) ) ;
#7065=CARTESIAN_POINT ( 'NONE',  ( 10.00000000000000000, -24.46385708179976604, -9.514709542737152859 ) ) ;
#7072=ORIENTED_EDGE ( 'NONE', *, *, #3039, .T. ) ;
#7083=CARTESIAN_POINT ( 'NONE',  ( 0.000000000000000000, 22.07705612348839708, 14.19907017806876048 ) ) ;
#7089=DIRECTION ( 'NONE',  ( -1.000000000000000000, -0.000000000000000000, 0.000000000000000000 ) ) ;
#7093=CARTESIAN_POINT ( 'NONE',  ( -10.00000000000000000, 0.000000000000000000, 0.000000000000000000 ) ) ;
#7115=ORIENTED_EDGE ( 'NONE', *, *, #10843, .T. ) ;
#7118=EDGE_CURVE ( 'NONE', #5630, #10460, #7417, .T. ) ;
#7125=VERTEX_POINT ( 'NONE', #17899 ) ;
#7136=DIRECTION ( 'NONE',  ( -1.000000000000000000, 0.000000000000000000, 0.000000000000000000 ) ) ;
#7150=LINE ( 'NONE', #5782, #3271 ) ;
#7158=CYLINDRICAL_SURFACE ( 'NONE', #3827, 12.00000000001200462 ) ;
#7176=VECTOR ( 'NONE', #18784, 1000.000000000000000 ) ;
#7179=LINE ( 'NONE', #2897, #15152 ) ;
#7191=CIRCLE ( 'NONE', #16923, 33.00000000003299760 ) ;
#7193=CIRCLE ( 'NONE', #837, 33.00000000003299760 ) ;
#7199=ORIENTED_EDGE ( 'NONE', *, *, #5486, .T. ) ;
#7220=AXIS2_PLACEMENT_3D ( 'NONE', #9365, #5264, #6708 ) ;
#7227=DIRECTION ( 'NONE',  ( 0.000000000000000000, 0.000000000000000000, 1.000000000000000000 ) ) ;
#7231=CARTESIAN_POINT ( 'NONE',  ( 0.000000000000000000, 0.000000000000000000, 0.000000000000000000 ) ) ;
#7242=AXIS2_PLACEMENT_3D ( 'NONE', #17105, #16813, #4055 ) ;
#7244=ORIENTED_EDGE ( 'NONE', *, *, #754, .T. ) ;
#7253=DIRECTION ( 'NONE',  ( 0.000000000000000000, -0.3090169943749349613, -0.9510565162951576390 ) ) ;
#7254=EDGE_CURVE ( 'NONE', #684, #38, #16735, .T. ) ;
#7259=LINE ( 'NONE', #8683, #5657 ) ;
#7264=FACE_OUTER_BOUND ( 'NONE', #4128, .T. ) ;
#7267=ORIENTED_EDGE ( 'NONE', *, *, #272, .T. ) ;
#7272=EDGE_CURVE ( 'NONE', #16587, #18040, #307, .T. ) ;
#7274=EDGE_CURVE ( 'NONE', #10666, #18659, #21, .T. ) ;
#7276=CARTESIAN_POINT ( 'NONE',  ( 50.00005079999999680, 6.799999999999999822, -1.500000000000000000 ) ) ;
#7278=CIRCLE ( 'NONE', #1794, 26.24900000002624978 ) ;
#7281=EDGE_CURVE ( 'NONE', #6583, #4502, #13393, .T. ) ;
#7285=DIRECTION ( 'NONE',  ( -1.000000000000000000, 0.000000000000000000, -0.000000000000000000 ) ) ;
#7287=CYLINDRICAL_SURFACE ( 'NONE', #7300, 33.00000000003299760 ) ;
#7292=ORIENTED_EDGE ( 'NONE', *, *, #744, .T. ) ;
#7294=AXIS2_PLACEMENT_3D ( 'NONE', #937, #11203, #9965 ) ;
#7295=LINE ( 'NONE', #17581, #16906 ) ;
#7296=CARTESIAN_POINT ( 'NONE',  ( 0.000000000000000000, 24.79895094899259789, 13.40641754777674421 ) ) ;
#7297=CARTESIAN_POINT ( 'NONE',  ( 0.000000000000000000, 12.18267823974751352, 25.42247726998019530 ) ) ;
#7300=AXIS2_PLACEMENT_3D ( 'NONE', #11380, #13107, #17387 ) ;
#7307=CIRCLE ( 'NONE', #14914, 33.00000000003299760 ) ;
#7312=ADVANCED_FACE ( 'NONE', ( #5673 ), #1572, .T. ) ;
#7313=CARTESIAN_POINT ( 'NONE',  ( 0.000000000000000000, -27.94286728106395756, 3.730438010304225394 ) ) ;
#7318=EDGE_LOOP ( 'NONE', ( #11275, #8171, #18426, #16369 ) ) ;
#7328=LINE ( 'NONE', #15908, #6574 ) ;
#7331=CYLINDRICAL_SURFACE ( 'NONE', #16023, 12.00000000001200462 ) ;
#7346=EDGE_LOOP ( 'NONE', ( #11154, #18223, #3566, #16661 ) ) ;
#7348=ORIENTED_EDGE ( 'NONE', *, *, #3913, .T. ) ;
#7353=VERTEX_POINT ( 'NONE', #17306 ) ;
#7360=CARTESIAN_POINT ( 'NONE',  ( -10.00000000000000000, 0.000000000000000000, 0.000000000000000000 ) ) ;
#7368=ADVANCED_FACE ( 'NONE', ( #2813 ), #12822, .T. ) ;
#7376=ADVANCED_FACE ( 'NONE', ( #2623 ), #7287, .T. ) ;
#7387=EDGE_CURVE ( 'NONE', #9886, #6276, #10041, .T. ) ;
#7391=ORIENTED_EDGE ( 'NONE', *, *, #16562, .T. ) ;
#7392=CARTESIAN_POINT ( 'NONE',  ( 10.00000000000000000, -26.20671763660629594, 1.489278925039428936 ) ) ;
#7395=CARTESIAN_POINT ( 'NONE',  ( 10.00000000000000000, -1.489278925039700052, 26.20671763660628173 ) ) ;
#7398=ORIENTED_EDGE ( 'NONE', *, *, #1151, .F. ) ;
#7405=EDGE_CURVE ( 'NONE', #12797, #13152, #9738, .T. ) ;
#7416=ORIENTED_EDGE ( 'NONE', *, *, #15357, .T. ) ;
#7417=LINE ( 'NONE', #13234, #2 ) ;
#7423=EDGE_CURVE ( 'NONE', #16256, #3146, #17638, .T. ) ;
#7427=VERTEX_POINT ( 'NONE', #1751 ) ;
#7439=CARTESIAN_POINT ( 'NONE',  ( 10.00000000000000000, -20.32630374611196800, 16.60877409751161693 ) ) ;
#7448=CARTESIAN_POINT ( 'NONE',  ( 10.00000000000000000, 0.000000000000000000, 0.000000000000000000 ) ) ;
#7454=AXIS2_PLACEMENT_3D ( 'NONE', #642, #9112, #10717 ) ;
#7455=CARTESIAN_POINT ( 'NONE',  ( 10.00000000000000000, 0.000000000000000000, 0.000000000000000000 ) ) ;
#7459=DIRECTION ( 'NONE',  ( 0.000000000000000000, -0.3090169943749349613, -0.9510565162951576390 ) ) ;
#7474=EDGE_CURVE ( 'NONE', #8506, #7504, #15148, .T. ) ;
#7476=DIRECTION ( 'NONE',  ( -1.000000000000000000, 0.000000000000000000, 0.000000000000000000 ) ) ;
#7496=DIRECTION ( 'NONE',  ( -0.000000000000000000, 1.000000000000000000, 0.000000000000000000 ) ) ;
#7499=EDGE_CURVE ( 'NONE', #16517, #7974, #14706, .T. ) ;
#7504=VERTEX_POINT ( 'NONE', #3098 ) ;
#7508=CYLINDRICAL_SURFACE ( 'NONE', #16033, 26.24900000002624978 ) ;
#7510=DIRECTION ( 'NONE',  ( -1.000000000000000000, -0.000000000000000000, -0.000000000000000000 ) ) ;
#7525=VERTEX_POINT ( 'NONE', #13386 ) ;
#7528=AXIS2_PLACEMENT_3D ( 'NONE', #14355, #11396, #4729 ) ;
#7537=ORIENTED_EDGE ( 'NONE', *, *, #6437, .F. ) ;
#7548=VECTOR ( 'NONE', #4311, 1000.000000000000000 ) ;
#7552=DIRECTION ( 'NONE',  ( 0.000000000000000000, 0.000000000000000000, 1.000000000000000000 ) ) ;
#7578=CARTESIAN_POINT ( 'NONE',  ( 10.00000000000000000, 27.94286728106393269, 15.73043801031642808 ) ) ;
#7582=DIRECTION ( 'NONE',  ( 0.000000000000000000, 0.000000000000000000, -1.000000000000000000 ) ) ;
#7586=AXIS2_PLACEMENT_3D ( 'NONE', #14949, #4475, #4658 ) ;
#7601=ORIENTED_EDGE ( 'NONE', *, *, #15532, .T. ) ;
#7607=DIRECTION ( 'NONE',  ( -1.000000000000000000, 0.000000000000000000, -0.000000000000000000 ) ) ;
#7615=EDGE_CURVE ( 'NONE', #34, #17821, #2062, .T. ) ;
#7625=LINE ( 'NONE', #17635, #7176 ) ;
#7630=LINE ( 'NONE', #3076, #5764 ) ;
#7632=CARTESIAN_POINT ( 'NONE',  ( 0.000000000000000000, 6.799999999999999822, -1.500000000000000000 ) ) ;
#7637=ORIENTED_EDGE ( 'NONE', *, *, #12616, .T. ) ;
#7639=DIRECTION ( 'NONE',  ( 0.000000000000000000, -0.5877852522924624790, -0.8090169943749551118 ) ) ;
#7644=FACE_OUTER_BOUND ( 'NONE', #15257, .T. ) ;
#7645=DIRECTION ( 'NONE',  ( 0.000000000000000000, 0.000000000000000000, 1.000000000000000000 ) ) ;
#7647=CARTESIAN_POINT ( 'NONE',  ( 0.000000000000000000, -9.514709542736730086, -24.46385708179993301 ) ) ;
#7663=ORIENTED_EDGE ( 'NONE', *, *, #10152, .F. ) ;
#7666=DIRECTION ( 'NONE',  ( -1.000000000000000000, 0.000000000000000000, 0.000000000000000000 ) ) ;
#7670=ORIENTED_EDGE ( 'NONE', *, *, #15700, .T. ) ;
#7678=CIRCLE ( 'NONE', #12563, 12.00000000001200462 ) ;
#7684=LINE ( 'NONE', #3046, #9573 ) ;
#7686=ORIENTED_EDGE ( 'NONE', *, *, #6894, .F. ) ;
#7688=AXIS2_PLACEMENT_3D ( 'NONE', #11193, #17023, #8343 ) ;
#7690=CARTESIAN_POINT ( 'NONE',  ( 10.00000000000000000, 9.514709542737238124, -24.46385708179973406 ) ) ;
#7692=ORIENTED_EDGE ( 'NONE', *, *, #725, .T. ) ;
#7693=VECTOR ( 'NONE', #3239, 1000.000000000000000 ) ;
#7695=ADVANCED_FACE ( 'NONE', ( #6796 ), #8132, .T. ) ;
#7696=DIRECTION ( 'NONE',  ( -1.000000000000000000, 0.000000000000000000, 0.000000000000000000 ) ) ;
#7698=ORIENTED_EDGE ( 'NONE', *, *, #9226, .F. ) ;
#7719=DIRECTION ( 'NONE',  ( -1.000000000000000000, 0.000000000000000000, -0.000000000000000000 ) ) ;
#7721=EDGE_CURVE ( 'NONE', #15269, #13370, #14237, .T. ) ;
#7727=DIRECTION ( 'NONE',  ( 0.000000000000000000, 0.000000000000000000, 1.000000000000000000 ) ) ;
#7736=ORIENTED_EDGE ( 'NONE', *, *, #12960, .F. ) ;
#7737=DIRECTION ( 'NONE',  ( -1.000000000000000000, -0.000000000000000000, 0.000000000000000000 ) ) ;
#7750=CARTESIAN_POINT ( 'NONE',  ( 0.000000000000000000, 0.000000000000000000, 0.000000000000000000 ) ) ;
#7763=ORIENTED_EDGE ( 'NONE', *, *, #6811, .F. ) ;
#7772=AXIS2_PLACEMENT_3D ( 'NONE', #2429, #13845, #18137 ) ;
#7784=DIRECTION ( 'NONE',  ( 0.000000000000000000, 0.000000000000000000, 1.000000000000000000 ) ) ;
#7796=CARTESIAN_POINT ( 'NONE',  ( 10.00000000000000000, 22.76987570971527575, 23.88582760061489552 ) ) ;
#7803=AXIS2_PLACEMENT_3D ( 'NONE', #11331, #10, #1338 ) ;
#7829=CARTESIAN_POINT ( 'NONE',  ( 10.00000000000000000, 6.799999999999999822, 0.000000000000000000 ) ) ;
#7830=AXIS2_PLACEMENT_3D ( 'NONE', #11391, #17211, #9969 ) ;
#7834=CARTESIAN_POINT ( 'NONE',  ( 0.000000000000000000, 0.000000000000000000, 0.000000000000000000 ) ) ;
#7837=CARTESIAN_POINT ( 'NONE',  ( 10.00000000000000000, -25.42247726998023083, 12.18267823974742470 ) ) ;
#7839=ORIENTED_EDGE ( 'NONE', *, *, #6682, .T. ) ;
#7852=DIRECTION ( 'NONE',  ( -1.000000000000000000, 0.000000000000000000, 0.000000000000000000 ) ) ;
#7855=AXIS2_PLACEMENT_3D ( 'NONE', #11621, #5718, #1340 ) ;
#7863=LINE ( 'NONE', #15206, #9777 ) ;
#7867=AXIS2_PLACEMENT_3D ( 'NONE', #12181, #10455, #14745 ) ;
#7868=CARTESIAN_POINT ( 'NONE',  ( 0.000000000000000000, 4.769696007084728073, -1.500000000000000000 ) ) ;
#7869=VERTEX_POINT ( 'NONE', #17921 ) ;
#7871=DIRECTION ( 'NONE',  ( -1.000000000000000000, 0.000000000000000000, 0.000000000000000000 ) ) ;
#7876=VERTEX_POINT ( 'NONE', #9154 ) ;
#7888=CARTESIAN_POINT ( 'NONE',  ( 0.000000000000000000, -19.44239304137360946, -20.41355805489636310 ) ) ;
#7889=ORIENTED_EDGE ( 'NONE', *, *, #15039, .F. ) ;
#7897=CARTESIAN_POINT ( 'NONE',  ( 10.00000000000000000, 13.40641754777665717, 24.79895094899264052 ) ) ;
#7902=CIRCLE ( 'NONE', #13094, 12.00000000001200107 ) ;
#7904=VERTEX_POINT ( 'NONE', #7439 ) ;
#7908=CARTESIAN_POINT ( 'NONE',  ( 0.000000000000000000, 19.44239304137375868, 20.41355805489622455 ) ) ;
#7911=CARTESIAN_POINT ( 'NONE',  ( 10.00000000000000000, 25.38428207620322752, 6.681932690257054830 ) ) ;
#7914=DIRECTION ( 'NONE',  ( -1.000000000000000000, 0.000000000000000000, 0.000000000000000000 ) ) ;
#7919=ORIENTED_EDGE ( 'NONE', *, *, #11923, .F. ) ;
#7921=ORIENTED_EDGE ( 'NONE', *, *, #9117, .F. ) ;
#7931=CARTESIAN_POINT ( 'NONE',  ( 0.000000000000000000, -4.381479206523217762, 32.70783759231085241 ) ) ;
#7950=VECTOR ( 'NONE', #8611, 1000.000000000000000 ) ;
#7960=ORIENTED_EDGE ( 'NONE', *, *, #2377, .F. ) ;
#7964=FILL_AREA_STYLE_COLOUR ( '', #13210 ) ;
#7966=ORIENTED_EDGE ( 'NONE', *, *, #5200, .F. ) ;
#7967=CARTESIAN_POINT ( 'NONE',  ( 10.00000000000000000, 29.75305054077492173, -14.27431201565494412 ) ) ;
#7968=ADVANCED_FACE ( 'NONE', ( #1917 ), #17549, .T. ) ;
#7974=VERTEX_POINT ( 'NONE', #7632 ) ;
#7975=CARTESIAN_POINT ( 'NONE',  ( 0.000000000000000000, 22.76987570971527575, 23.88582760061489552 ) ) ;
#7977=DIRECTION ( 'NONE',  ( -1.000000000000000000, 0.000000000000000000, 0.000000000000000000 ) ) ;
#7978=VERTEX_POINT ( 'NONE', #15063 ) ;
#7984=DIRECTION ( 'NONE',  ( 0.000000000000000000, -0.9510565162951565288, 0.3090169943749384029 ) ) ;
#7986=ORIENTED_EDGE ( 'NONE', *, *, #13791, .T. ) ;
#7990=EDGE_CURVE ( 'NONE', #15870, #9667, #2688, .T. ) ;
#7997=CYLINDRICAL_SURFACE ( 'NONE', #15123, 12.00000000001200462 ) ;
#8001=VERTEX_POINT ( 'NONE', #12580 ) ;
#8003=ADVANCED_FACE ( 'NONE', ( #3820 ), #9623, .T. ) ;
#8005=DIRECTION ( 'NONE',  ( -1.000000000000000000, -0.000000000000000000, 0.000000000000000000 ) ) ;
#8006=ORIENTED_EDGE ( 'NONE', *, *, #6682, .F. ) ;
#8013=DIRECTION ( 'NONE',  ( -1.000000000000000000, -0.000000000000000000, -0.000000000000000000 ) ) ;
#8017=AXIS2_PLACEMENT_3D ( 'NONE', #12801, #14324, #9934 ) ;
#8027=ORIENTED_EDGE ( 'NONE', *, *, #7281, .T. ) ;
#8028=ORIENTED_EDGE ( 'NONE', *, *, #3757, .F. ) ;
#8043=UNCERTAINTY_MEASURE_WITH_UNIT (LENGTH_MEASURE( 1.000000000000000082E-05 ), #1180, 'distance_accuracy_value', 'NONE');
#8050=DIRECTION ( 'NONE',  ( 0.000000000000000000, 0.000000000000000000, -1.000000000000000000 ) ) ;
#8060=DIRECTION ( 'NONE',  ( 0.000000000000000000, 0.000000000000000000, -1.000000000000000000 ) ) ;
#8061=AXIS2_PLACEMENT_3D ( 'NONE', #16641, #650, #6452 ) ;
#8063=AXIS2_PLACEMENT_3D ( 'NONE', #11557, #14404, #4127 ) ;
#8064=ORIENTED_EDGE ( 'NONE', *, *, #7474, .T. ) ;
#8065=EDGE_CURVE ( 'NONE', #4831, #3895, #13949, .T. ) ;
#8067=EDGE_CURVE ( 'NONE', #4436, #10666, #2287, .T. ) ;
#8068=EDGE_CURVE ( 'NONE', #4319, #7125, #8106, .T. ) ;
#8076=EDGE_CURVE ( 'NONE', #7978, #1162, #8166, .T. ) ;
#8079=VECTOR ( 'NONE', #15889, 1000.000000000000000 ) ;
#8082=CARTESIAN_POINT ( 'NONE',  ( 10.00000000000000000, 0.000000000000000000, 0.000000000000000000 ) ) ;
#8086=CIRCLE ( 'NONE', #3826, 12.00000000001200462 ) ;
#8106=LINE ( 'NONE', #9728, #8472 ) ;
#8113=AXIS2_PLACEMENT_3D ( 'NONE', #9898, #12771, #15719 ) ;
#8116=FACE_OUTER_BOUND ( 'NONE', #2284, .T. ) ;
#8119=DIRECTION ( 'NONE',  ( -1.000000000000000000, -0.000000000000000000, -0.000000000000000000 ) ) ;
#8128=DIRECTION ( 'NONE',  ( 0.000000000000000000, 0.000000000000000000, 1.000000000000000000 ) ) ;
#8129=VERTEX_POINT ( 'NONE', #12487 ) ;
#8132=CYLINDRICAL_SURFACE ( 'NONE', #17871, 33.00000000003299760 ) ;
#8140=AXIS2_PLACEMENT_3D ( 'NONE', #18760, #7510, #15991 ) ;
#8144=CARTESIAN_POINT ( 'NONE',  ( 10.00000000000000000, 20.41355805489643060, -19.44239304137353841 ) ) ;
#8149=CIRCLE ( 'NONE', #14837, 26.24900000002624978 ) ;
#8159=ORIENTED_EDGE ( 'NONE', *, *, #18080, .T. ) ;
#8161=DIRECTION ( 'NONE',  ( -1.000000000000000000, 0.000000000000000000, 0.000000000000000000 ) ) ;
#8166=CIRCLE ( 'NONE', #9990, 12.00000000001200817 ) ;
#8170=CARTESIAN_POINT ( 'NONE',  ( 10.00000000000000000, -5.086963483077402870, 27.72801475327280585 ) ) ;
#8171=ORIENTED_EDGE ( 'NONE', *, *, #6093, .F. ) ;
#8178=CARTESIAN_POINT ( 'NONE',  ( 4.999999999999999112, -4.381479206523219538, 32.70783759231085241 ) ) ;
#8185=CIRCLE ( 'NONE', #10002, 33.00000000003299760 ) ;
#8189=AXIS2_PLACEMENT_3D ( 'NONE', #2381, #3529, #9324 ) ;
#8190=VECTOR ( 'NONE', #1523, 1000.000000000000000 ) ;
#8208=DIRECTION ( 'NONE',  ( -1.000000000000000000, 0.000000000000000000, 0.000000000000000000 ) ) ;
#8215=EDGE_CURVE ( 'NONE', #205, #6839, #1786, .T. ) ;
#8218=ADVANCED_FACE ( 'NONE', ( #13062 ), #10012, .T. ) ;
#8229=DIRECTION ( 'NONE',  ( -1.000000000000000000, 0.000000000000000000, 0.000000000000000000 ) ) ;
#8230=ORIENTED_EDGE ( 'NONE', *, *, #10736, .F. ) ;
#8236=ORIENTED_EDGE ( 'NONE', *, *, #16562, .F. ) ;
#8240=ORIENTED_EDGE ( 'NONE', *, *, #1019, .F. ) ;
#8251=CARTESIAN_POINT ( 'NONE',  ( -10.00000000000000000, 0.000000000000000000, 0.000000000000000000 ) ) ;
#8252=CARTESIAN_POINT ( 'NONE',  ( 10.00000000000000000, 22.07705612348840063, 14.19907017806876404 ) ) ;
#8261=LINE ( 'NONE', #1118, #11561 ) ;
#8267=CARTESIAN_POINT ( 'NONE',  ( 10.00000000000000000, -19.44239304137390434, 20.41355805489607889 ) ) ;
#8276=CARTESIAN_POINT ( 'NONE',  ( 5.000000000000000000, -32.70783759231083820, -4.381479206523334113 ) ) ;
#8278=ORIENTED_EDGE ( 'NONE', *, *, #2375, .T. ) ;
#8289=LINE ( 'NONE', #18284, #2328 ) ;
#8295=CARTESIAN_POINT ( 'NONE',  ( 5.000000000000000000, 29.75305054077492173, -14.27431201565494767 ) ) ;
#8302=CARTESIAN_POINT ( 'NONE',  ( 10.00000000000000000, -27.72801475327278453, 6.913036516934497833 ) ) ;
#8321=ORIENTED_EDGE ( 'NONE', *, *, #13363, .F. ) ;
#8324=AXIS2_PLACEMENT_3D ( 'NONE', #1571, #1381, #3008 ) ;
#8328=VERTEX_POINT ( 'NONE', #196 ) ;
#8343=DIRECTION ( 'NONE',  ( 0.000000000000000000, 0.000000000000000000, 1.000000000000000000 ) ) ;
#8351=CARTESIAN_POINT ( 'NONE',  ( 0.000000000000000000, -3.730438010304114371, -27.94286728106396822 ) ) ;
#8366=ORIENTED_EDGE ( 'NONE', *, *, #6267, .F. ) ;
#8368=CYLINDRICAL_SURFACE ( 'NONE', #4459, 12.00000000001200462 ) ;
#8375=EDGE_CURVE ( 'NONE', #5515, #14782, #3006, .T. ) ;
#8380=CARTESIAN_POINT ( 'NONE',  ( 0.000000000000000000, 23.88582760061514776, -22.76987570971501640 ) ) ;
#8385=LINE ( 'NONE', #9618, #17884 ) ;
#8387=CIRCLE ( 'NONE', #12329, 5.000000000000000000 ) ;
#8392=LINE ( 'NONE', #9263, #1992 ) ;
#8397=EDGE_LOOP ( 'NONE', ( #1884, #11855, #1312, #662 ) ) ;
#8400=ORIENTED_EDGE ( 'NONE', *, *, #16766, .T. ) ;
#8402=EDGE_LOOP ( 'NONE', ( #6830, #17340, #16217, #11165 ) ) ;
#8407=VECTOR ( 'NONE', #10424, 1000.000000000000000 ) ;
#8413=LINE ( 'NONE', #4132, #13507 ) ;
#8426=AXIS2_PLACEMENT_3D ( 'NONE', #16759, #12654, #3710 ) ;
#8428=DIRECTION ( 'NONE',  ( 0.000000000000000000, -0.3090169943749348502, -0.9510565162951576390 ) ) ;
#8433=DIRECTION ( 'NONE',  ( -1.000000000000000000, 0.000000000000000000, -0.000000000000000000 ) ) ;
#8435=DIRECTION ( 'NONE',  ( 1.000000000000000000, 0.000000000000000000, 0.000000000000000000 ) ) ;
#8448=EDGE_CURVE ( 'NONE', #3135, #16274, #8185, .T. ) ;
#8452=EDGE_CURVE ( 'NONE', #726, #7504, #11717, .T. ) ;
#8456=ORIENTED_EDGE ( 'NONE', *, *, #11861, .T. ) ;
#8458=CARTESIAN_POINT ( 'NONE',  ( 0.000000000000000000, 0.000000000000000000, 0.000000000000000000 ) ) ;
#8471=CIRCLE ( 'NONE', #12110, 33.00000000003299760 ) ;
#8472=VECTOR ( 'NONE', #15539, 1000.000000000000000 ) ;
#8491=DIRECTION ( 'NONE',  ( -1.000000000000000000, 0.000000000000000000, 0.000000000000000000 ) ) ;
#8492=EDGE_CURVE ( 'NONE', #11257, #3135, #13645, .T. ) ;
#8498=CYLINDRICAL_SURFACE ( 'NONE', #9310, 12.00000000001200817 ) ;
#8499=LINE ( 'NONE', #18389, #9436 ) ;
#8500=VERTEX_POINT ( 'NONE', #3625 ) ;
#8506=VERTEX_POINT ( 'NONE', #7796 ) ;
#8513=LINE ( 'NONE', #11177, #5378 ) ;
#8514=EDGE_LOOP ( 'NONE', ( #7348, #8850, #12294, #12989 ) ) ;
#8515=AXIS2_PLACEMENT_3D ( 'NONE', #928, #15580, #16916 ) ;
#8516=CIRCLE ( 'NONE', #10645, 12.00000000001200284 ) ;
#8523=ADVANCED_FACE ( 'NONE', ( #16761 ), #9511, .T. ) ;
#8527=CARTESIAN_POINT ( 'NONE',  ( 10.00000000000000000, 27.72801475327282361, -5.086963483077305170 ) ) ;
#8543=CIRCLE ( 'NONE', #17377, 12.00000000001200462 ) ;
#8545=DIRECTION ( 'NONE',  ( -1.000000000000000000, -0.000000000000000000, -0.000000000000000000 ) ) ;
#8546=EDGE_LOOP ( 'NONE', ( #1603, #7960, #10750, #6371 ) ) ;
#8550=EDGE_CURVE ( 'NONE', #944, #4267, #3799, .T. ) ;
#8555=CYLINDRICAL_SURFACE ( 'NONE', #4175, 33.00000000003299760 ) ;
#8564=EDGE_LOOP ( 'NONE', ( #9795, #4795, #4624, #978 ) ) ;
#8573=ORIENTED_EDGE ( 'NONE', *, *, #10399, .T. ) ;
#8574=CARTESIAN_POINT ( 'NONE',  ( 5.000000000000000000, 29.03656532225563680, 15.68049343256006800 ) ) ;
#8592=DIRECTION ( 'NONE',  ( -1.000000000000000000, -0.000000000000000000, -0.000000000000000000 ) ) ;
#8611=DIRECTION ( 'NONE',  ( -1.000000000000000000, 0.000000000000000000, 0.000000000000000000 ) ) ;
#8614=DIRECTION ( 'NONE',  ( -1.000000000000000000, 0.000000000000000000, 0.000000000000000000 ) ) ;
#8619=DIRECTION ( 'NONE',  ( -1.000000000000000000, 0.000000000000000000, -0.000000000000000000 ) ) ;
#8620=VERTEX_POINT ( 'NONE', #12275 ) ;
#8637=DIRECTION ( 'NONE',  ( -1.000000000000000000, -0.000000000000000000, -0.000000000000000000 ) ) ;
#8640=DIRECTION ( 'NONE',  ( 0.000000000000000000, 0.000000000000000000, -1.000000000000000000 ) ) ;
#8641=ORIENTED_EDGE ( 'NONE', *, *, #8067, .T. ) ;
#8646=CARTESIAN_POINT ( 'NONE',  ( 10.00000000000000000, -26.20671763660627462, -1.489278925039791535 ) ) ;
#8649=ORIENTED_EDGE ( 'NONE', *, *, #1098, .T. ) ;
#8654=DIRECTION ( 'NONE',  ( -1.000000000000000000, -0.000000000000000000, -0.000000000000000000 ) ) ;
#8657=DIRECTION ( 'NONE',  ( -1.000000000000000000, -0.000000000000000000, 0.000000000000000000 ) ) ;
#8662=CARTESIAN_POINT ( 'NONE',  ( 0.000000000000000000, -1.489278925039337675, -26.20671763660630305 ) ) ;
#8668=AXIS2_PLACEMENT_3D ( 'NONE', #3326, #15026, #3219 ) ;
#8674=DIRECTION ( 'NONE',  ( 0.000000000000000000, -0.5877852522924804646, 0.8090169943749421222 ) ) ;
#8679=EDGE_CURVE ( 'NONE', #4486, #4831, #10082, .T. ) ;
#8683=CARTESIAN_POINT ( 'NONE',  ( 5.000000000000000000, 22.76987570971561681, -23.88582760061456511 ) ) ;
#8687=DIRECTION ( 'NONE',  ( -1.000000000000000000, 0.000000000000000000, -0.000000000000000000 ) ) ;
#8711=DIRECTION ( 'NONE',  ( 0.000000000000000000, -1.000000000000000000, 0.000000000000000000 ) ) ;
#8712=EDGE_LOOP ( 'NONE', ( #11403, #9805, #2656, #3094 ) ) ;
#8716=CIRCLE ( 'NONE', #4165, 33.00000000003299760 ) ;
#8718=ADVANCED_FACE ( 'NONE', ( #17056 ), #17335, .T. ) ;
#8720=DIRECTION ( 'NONE',  ( -1.000000000000000000, -0.000000000000000000, -0.000000000000000000 ) ) ;
#8721=DIRECTION ( 'NONE',  ( 0.000000000000000000, 0.000000000000000000, -1.000000000000000000 ) ) ;
#8725=ORIENTED_EDGE ( 'NONE', *, *, #2486, .T. ) ;
#8744=LINE ( 'NONE', #11616, #13592 ) ;
#8746=PLANE ( 'NONE',  #5390 ) ;
#8748=CYLINDRICAL_SURFACE ( 'NONE', #8140, 33.00000000003299760 ) ;
#8749=CARTESIAN_POINT ( 'NONE',  ( 10.00000000000000000, 19.44239304137375868, 20.41355805489622455 ) ) ;
#8756=ADVANCED_FACE ( 'NONE', ( #14179 ), #6946, .T. ) ;
#8757=CARTESIAN_POINT ( 'NONE',  ( 0.000000000000000000, 27.94286728106398243, -3.730438010304017116 ) ) ;
#8759=EDGE_CURVE ( 'NONE', #11810, #17358, #6840, .T. ) ;
#8771=AXIS2_PLACEMENT_3D ( 'NONE', #5727, #11544, #10105 ) ;
#8785=ADVANCED_FACE ( 'NONE', ( #17690 ), #5969, .T. ) ;
#8791=VECTOR ( 'NONE', #5707, 1000.000000000000000 ) ;
#8799=CARTESIAN_POINT ( 'NONE',  ( 4.999999999999999112, -32.70783759231089505, 4.381479206522875813 ) ) ;
#8810=ORIENTED_EDGE ( 'NONE', *, *, #10356, .T. ) ;
#8812=EDGE_CURVE ( 'NONE', #9886, #9496, #16079, .T. ) ;
#8816=DIRECTION ( 'NONE',  ( -1.000000000000000000, 0.000000000000000000, -0.000000000000000000 ) ) ;
#8819=ORIENTED_EDGE ( 'NONE', *, *, #13791, .F. ) ;
#8835=AXIS2_PLACEMENT_3D ( 'NONE', #3436, #12455, #477 ) ;
#8838=DIRECTION ( 'NONE',  ( -1.000000000000000000, 0.000000000000000000, 0.000000000000000000 ) ) ;
#8844=CYLINDRICAL_SURFACE ( 'NONE', #11523, 12.00000000001200107 ) ;
#8846=DIRECTION ( 'NONE',  ( 0.000000000000000000, 0.5877852522924742473, -0.8090169943749465631 ) ) ;
#8847=VERTEX_POINT ( 'NONE', #17776 ) ;
#8850=ORIENTED_EDGE ( 'NONE', *, *, #13196, .F. ) ;
#8851=CARTESIAN_POINT ( 'NONE',  ( 5.000000000000000000, 23.88582760061481380, 22.76987570971536101 ) ) ;
#8868=DIRECTION ( 'NONE',  ( -1.000000000000000000, 0.000000000000000000, 0.000000000000000000 ) ) ;
#8879=CYLINDRICAL_SURFACE ( 'NONE', #2016, 26.24900000002624978 ) ;
#8886=DIRECTION ( 'NONE',  ( 0.000000000000000000, 0.000000000000000000, 1.000000000000000000 ) ) ;
#8889=VERTEX_POINT ( 'NONE', #15219 ) ;
#8895=DIRECTION ( 'NONE',  ( 0.000000000000000000, 0.000000000000000000, 1.000000000000000000 ) ) ;
#8931=EDGE_CURVE ( 'NONE', #3758, #16169, #646, .T. ) ;
#8937=CARTESIAN_POINT ( 'NONE',  ( 10.00000000000000000, -24.79895094899250196, -13.40641754777691830 ) ) ;
#8938=ORIENTED_EDGE ( 'NONE', *, *, #5464, .T. ) ;
#8942=ADVANCED_FACE ( 'NONE', ( #3405 ), #13599, .T. ) ;
#8950=CARTESIAN_POINT ( 'NONE',  ( -10.00000000000000000, 0.000000000000000000, 0.000000000000000000 ) ) ;
#8963=AXIS2_PLACEMENT_3D ( 'NONE', #5598, #11399, #14900 ) ;
#8965=FACE_OUTER_BOUND ( 'NONE', #6756, .T. ) ;
#8972=CARTESIAN_POINT ( 'NONE',  ( 10.00000000000000000, 14.19907017806900207, -22.07705612348824076 ) ) ;
#9007=VERTEX_POINT ( 'NONE', #7967 ) ;
#9014=VECTOR ( 'NONE', #3738, 1000.000000000000000 ) ;
#9024=ORIENTED_EDGE ( 'NONE', *, *, #7254, .T. ) ;
#9026=CARTESIAN_POINT ( 'NONE',  ( 10.00000000000000000, -12.18267823974769293, 25.42247726998010648 ) ) ;
#9030=DIRECTION ( 'NONE',  ( -1.000000000000000000, 0.000000000000000000, 0.000000000000000000 ) ) ;
#9033=ORIENTED_EDGE ( 'NONE', *, *, #16822, .F. ) ;
#9036=ORIENTED_EDGE ( 'NONE', *, *, #1391, .F. ) ;
#9038=DIRECTION ( 'NONE',  ( 0.000000000000000000, 0.000000000000000000, 1.000000000000000000 ) ) ;
#9040=AXIS2_PLACEMENT_3D ( 'NONE', #15034, #1978, #7784 ) ;
#9043=ADVANCED_FACE ( 'NONE', ( #14260 ), #6919, .T. ) ;
#9046=CARTESIAN_POINT ( 'NONE',  ( 10.00000000000000000, 4.381479206522985059, 32.70783759231087373 ) ) ;
#9055=EDGE_LOOP ( 'NONE', ( #1662, #1441, #13237, #6355 ) ) ;
#9057=DIRECTION ( 'NONE',  ( 0.000000000000000000, -0.5877852522924804646, 0.8090169943749421222 ) ) ;
#9072=FACE_OUTER_BOUND ( 'NONE', #10678, .T. ) ;
#9080=DIRECTION ( 'NONE',  ( -1.000000000000000000, 0.000000000000000000, -0.000000000000000000 ) ) ;
#9096=DIRECTION ( 'NONE',  ( 1.000000000000000000, 0.000000000000000000, 0.000000000000000000 ) ) ;
#9099=ORIENTED_EDGE ( 'NONE', *, *, #16702, .T. ) ;
#9100=EDGE_CURVE ( 'NONE', #6853, #3758, #18544, .T. ) ;
#9101=CYLINDRICAL_SURFACE ( 'NONE', #9157, 12.00000000001200462 ) ;
#9105=VERTEX_POINT ( 'NONE', #18631 ) ;
#9112=DIRECTION ( 'NONE',  ( -1.000000000000000000, -0.000000000000000000, -0.000000000000000000 ) ) ;
#9117=EDGE_CURVE ( 'NONE', #11652, #7353, #8261, .T. ) ;
#9120=VERTEX_POINT ( 'NONE', #3978 ) ;
#9129=FACE_OUTER_BOUND ( 'NONE', #14186, .T. ) ;
#9137=DIRECTION ( 'NONE',  ( 0.000000000000000000, 0.000000000000000000, 1.000000000000000000 ) ) ;
#9141=AXIS2_PLACEMENT_3D ( 'NONE', #17084, #11053, #16879 ) ;
#9154=CARTESIAN_POINT ( 'NONE',  ( 0.000000000000000000, -23.88582760061497368, 22.76987570971518338 ) ) ;
#9157=AXIS2_PLACEMENT_3D ( 'NONE', #17484, #11682, #14722 ) ;
#9158=ORIENTED_EDGE ( 'NONE', *, *, #4637, .F. ) ;
#9161=DIRECTION ( 'NONE',  ( -1.000000000000000000, 0.000000000000000000, 0.000000000000000000 ) ) ;
#9165=CARTESIAN_POINT ( 'NONE',  ( 10.00000000000000000, 0.000000000000000000, 26.24900000002624978 ) ) ;
#9167=CARTESIAN_POINT ( 'NONE',  ( -10.00000000000000000, 0.000000000000000000, 0.000000000000000000 ) ) ;
#9171=ORIENTED_EDGE ( 'NONE', *, *, #12856, .F. ) ;
#9192=DIRECTION ( 'NONE',  ( -1.000000000000000000, -0.000000000000000000, -0.000000000000000000 ) ) ;
#9204=AXIS2_PLACEMENT_3D ( 'NONE', #8458, #231, #15598 ) ;
#9214=VECTOR ( 'NONE', #11088, 1000.000000000000000 ) ;
#9222=CARTESIAN_POINT ( 'NONE',  ( 10.00000000000000000, 27.94286728106398243, -3.730438010304017116 ) ) ;
#9226=EDGE_CURVE ( 'NONE', #6022, #10989, #2112, .T. ) ;
#9228=EDGE_CURVE ( 'NONE', #941, #5630, #4548, .T. ) ;
#9230=VERTEX_POINT ( 'NONE', #6409 ) ;
#9234=FACE_OUTER_BOUND ( 'NONE', #17725, .T. ) ;
#9235=DIRECTION ( 'NONE',  ( -1.000000000000000000, -0.000000000000000000, -0.000000000000000000 ) ) ;
#9248=EDGE_LOOP ( 'NONE', ( #16711, #2100, #8641, #12134 ) ) ;
#9254=CIRCLE ( 'NONE', #1064, 12.00000000001200640 ) ;
#9263=CARTESIAN_POINT ( 'NONE',  ( 5.000000000000000000, -32.46095361140688595, -5.940243314904557259 ) ) ;
#9266=ORIENTED_EDGE ( 'NONE', *, *, #14347, .F. ) ;
#9281=AXIS2_PLACEMENT_3D ( 'NONE', #13396, #9096, #343 ) ;
#9283=CARTESIAN_POINT ( 'NONE',  ( 0.000000000000000000, 0.000000000000000000, 0.000000000000000000 ) ) ;
#9296=AXIS2_PLACEMENT_3D ( 'NONE', #16499, #9161, #7727 ) ;
#9300=ORIENTED_EDGE ( 'NONE', *, *, #2489, .F. ) ;
#9310=AXIS2_PLACEMENT_3D ( 'NONE', #25, #14486, #9917 ) ;
#9312=ORIENTED_EDGE ( 'NONE', *, *, #10736, .T. ) ;
#9319=AXIS2_PLACEMENT_3D ( 'NONE', #8082, #15235, #11316 ) ;
#9324=DIRECTION ( 'NONE',  ( 0.000000000000000000, 0.5877852522924686962, 0.8090169943749507819 ) ) ;
#9329=DIRECTION ( 'NONE',  ( 0.000000000000000000, 0.000000000000000000, 1.000000000000000000 ) ) ;
#9332=VERTEX_POINT ( 'NONE', #12428 ) ;
#9334=CIRCLE ( 'NONE', #2050, 12.00000000001200640 ) ;
#9339=AXIS2_PLACEMENT_3D ( 'NONE', #5507, #11306, #3985 ) ;
#9341=EDGE_CURVE ( 'NONE', #10019, #9230, #7902, .T. ) ;
#9345=CIRCLE ( 'NONE', #864, 12.00000000001200284 ) ;
#9349=DIRECTION ( 'NONE',  ( -1.000000000000000000, -0.000000000000000000, 0.000000000000000000 ) ) ;
#9365=CARTESIAN_POINT ( 'NONE',  ( 10.00000000000000000, 0.000000000000000000, 0.000000000000000000 ) ) ;
#9370=DIRECTION ( 'NONE',  ( 0.000000000000000000, -1.000000000000000000, -1.040834085585042960E-14 ) ) ;
#9375=CIRCLE ( 'NONE', #6023, 26.24900000002625333 ) ;
#9386=ORIENTED_EDGE ( 'NONE', *, *, #11285, .T. ) ;
#9387=AXIS2_PLACEMENT_3D ( 'NONE', #15603, #6462, #16073 ) ;
#9394=ORIENTED_EDGE ( 'NONE', *, *, #1042, .F. ) ;
#9403=ORIENTED_EDGE ( 'NONE', *, *, #18434, .F. ) ;
#9408=CARTESIAN_POINT ( 'NONE',  ( 0.000000000000000000, 1.489278925039520640, 26.20671763660629239 ) ) ;
#9413=DIRECTION ( 'NONE',  ( -1.000000000000000000, -0.000000000000000000, 0.000000000000000000 ) ) ;
#9417=FACE_OUTER_BOUND ( 'NONE', #18141, .T. ) ;
#9420=DIRECTION ( 'NONE',  ( -1.000000000000000000, 0.000000000000000000, 0.000000000000000000 ) ) ;
#9428=DIRECTION ( 'NONE',  ( -1.000000000000000000, 0.000000000000000000, 0.000000000000000000 ) ) ;
#9436=VECTOR ( 'NONE', #4218, 1000.000000000000000 ) ;
#9441=ORIENTED_EDGE ( 'NONE', *, *, #9947, .T. ) ;
#9446=DIRECTION ( 'NONE',  ( -1.000000000000000000, 0.000000000000000000, -0.000000000000000000 ) ) ;
#9453=DIRECTION ( 'NONE',  ( 0.000000000000000000, 0.000000000000000000, 1.000000000000000000 ) ) ;
#9456=ORIENTED_EDGE ( 'NONE', *, *, #10220, .F. ) ;
#9457=EDGE_CURVE ( 'NONE', #923, #11328, #7307, .T. ) ;
#9466=ORIENTED_EDGE ( 'NONE', *, *, #5525, .T. ) ;
#9473=CARTESIAN_POINT ( 'NONE',  ( 0.000000000000000000, 24.79895094899259789, -13.40641754777674421 ) ) ;
#9478=DIRECTION ( 'NONE',  ( -1.000000000000000000, 0.000000000000000000, 0.000000000000000000 ) ) ;
#9484=LINE ( 'NONE', #5100, #9214 ) ;
#9489=ORIENTED_EDGE ( 'NONE', *, *, #10036, .T. ) ;
#9491=EDGE_CURVE ( 'NONE', #3305, #684, #12163, .T. ) ;
#9496=VERTEX_POINT ( 'NONE', #11575 ) ;
#9500=DIRECTION ( 'NONE',  ( -1.000000000000000000, 0.000000000000000000, 0.000000000000000000 ) ) ;
#9502=FACE_OUTER_BOUND ( 'NONE', #18204, .T. ) ;
#9503=EDGE_LOOP ( 'NONE', ( #1860, #17696, #6357, #7736 ) ) ;
#9511=CYLINDRICAL_SURFACE ( 'NONE', #13959, 12.00000000001200462 ) ;
#9513=CARTESIAN_POINT ( 'NONE',  ( 10.00000000000000000, 0.000000000000000000, 0.000000000000000000 ) ) ;
#9516=ORIENTED_EDGE ( 'NONE', *, *, #3913, .F. ) ;
#9524=CARTESIAN_POINT ( 'NONE',  ( 10.00000000000000000, 0.000000000000000000, 0.000000000000000000 ) ) ;
#9529=ADVANCED_FACE ( 'NONE', ( #133 ), #15941, .T. ) ;
#9532=ADVANCED_FACE ( 'NONE', ( #8965 ), #1560, .T. ) ;
#9535=LINE ( 'NONE', #16591, #9014 ) ;
#9536=CARTESIAN_POINT ( 'NONE',  ( 0.000000000000000000, -6.681932690257145424, 25.38428207620320265 ) ) ;
#9538=DIRECTION ( 'NONE',  ( -1.000000000000000000, -0.000000000000000000, -0.000000000000000000 ) ) ;
#9541=DIRECTION ( 'NONE',  ( 0.000000000000000000, -0.8090169943749402348, -0.5877852522924830181 ) ) ;
#9548=DIRECTION ( 'NONE',  ( 0.000000000000000000, 0.000000000000000000, 1.000000000000000000 ) ) ;
#9550=ORIENTED_EDGE ( 'NONE', *, *, #16572, .F. ) ;
#9560=ORIENTED_EDGE ( 'NONE', *, *, #8065, .F. ) ;
#9562=EDGE_LOOP ( 'NONE', ( #9266, #16820, #3644, #3899 ) ) ;
#9563=EDGE_CURVE ( 'NONE', #7010, #1366, #8516, .T. ) ;
#9573=VECTOR ( 'NONE', #16088, 1000.000000000000000 ) ;
#9582=CIRCLE ( 'NONE', #1672, 12.00000000001200640 ) ;
#9599=ORIENTED_EDGE ( 'NONE', *, *, #2507, .F. ) ;
#9605=ADVANCED_FACE ( 'NONE', ( #4512 ), #10323, .T. ) ;
#9618=CARTESIAN_POINT ( 'NONE',  ( 4.999999999999999112, -5.940243314903991489, -32.46095361140699254 ) ) ;
#9623=CYLINDRICAL_SURFACE ( 'NONE', #11813, 12.00000000001200462 ) ;
#9630=VERTEX_POINT ( 'NONE', #4689 ) ;
#9631=CIRCLE ( 'NONE', #12359, 12.00000000001200284 ) ;
#9642=DIRECTION ( 'NONE',  ( -1.000000000000000000, -0.000000000000000000, 0.000000000000000000 ) ) ;
#9648=DIRECTION ( 'NONE',  ( -1.000000000000000000, 0.000000000000000000, 0.000000000000000000 ) ) ;
#9656=DIRECTION ( 'NONE',  ( 0.000000000000000000, 0.5877852522924684742, 0.8090169943749507819 ) ) ;
#9660=DIRECTION ( 'NONE',  ( 0.000000000000000000, 0.8090169943749446757, 0.5877852522924769119 ) ) ;
#9663=CARTESIAN_POINT ( 'NONE',  ( 0.000000000000000000, 14.19907017806868588, 22.07705612348844326 ) ) ;
#9667=VERTEX_POINT ( 'NONE', #9536 ) ;
#9668=AXIS2_PLACEMENT_3D ( 'NONE', #2008, #5919, #4505 ) ;
#9674=ORIENTED_EDGE ( 'NONE', *, *, #11723, .T. ) ;
#9678=ORIENTED_EDGE ( 'NONE', *, *, #18266, .T. ) ;
#9680=AXIS2_PLACEMENT_3D ( 'NONE', #1865, #7666, #10710 ) ;
#9683=EDGE_CURVE ( 'NONE', #16517, #8328, #10871, .T. ) ;
#9690=ORIENTED_EDGE ( 'NONE', *, *, #15356, .F. ) ;
#9697=ADVANCED_FACE ( 'NONE', ( #10965 ), #14982, .T. ) ;
#9719=DIRECTION ( 'NONE',  ( 1.000000000000000000, -0.000000000000000000, -0.000000000000000000 ) ) ;
#9728=CARTESIAN_POINT ( 'NONE',  ( 10.00000000000000000, -24.46385708179990459, 9.514709542736804693 ) ) ;
#9730=DIRECTION ( 'NONE',  ( 0.000000000000000000, 1.000000000000000000, 3.469446951950143595E-15 ) ) ;
#9738=CIRCLE ( 'NONE', #14305, 12.00000000001200640 ) ;
#9743=DIRECTION ( 'NONE',  ( -1.000000000000000000, 0.000000000000000000, 0.000000000000000000 ) ) ;
#9746=DIRECTION ( 'NONE',  ( -1.000000000000000000, 0.000000000000000000, 0.000000000000000000 ) ) ;
#9757=ORIENTED_EDGE ( 'NONE', *, *, #17263, .T. ) ;
#9767=ORIENTED_EDGE ( 'NONE', *, *, #2146, .T. ) ;
#9768=CARTESIAN_POINT ( 'NONE',  ( 0.000000000000000000, -29.75305054077462330, -14.27431201565557117 ) ) ;
#9772=ORIENTED_EDGE ( 'NONE', *, *, #13675, .F. ) ;
#9777=VECTOR ( 'NONE', #724, 1000.000000000000000 ) ;
#9782=CARTESIAN_POINT ( 'NONE',  ( 50.00005079999999680, 0.000000000000000000, 5.000000000000000000 ) ) ;
#9785=UNCERTAINTY_MEASURE_WITH_UNIT (LENGTH_MEASURE( 1.000000000000000082E-05 ), #85, 'distance_accuracy_value', 'NONE');
#9787=CARTESIAN_POINT ( 'NONE',  ( 5.000000000000000000, 29.03656532225586062, -15.68049343255964523 ) ) ;
#9789=ORIENTED_EDGE ( 'NONE', *, *, #16977, .T. ) ;
#9790=DIRECTION ( 'NONE',  ( -1.000000000000000000, -0.000000000000000000, -0.000000000000000000 ) ) ;
#9792=LINE ( 'NONE', #8276, #11208 ) ;
#9793=DIRECTION ( 'NONE',  ( 1.000000000000000000, 0.000000000000000000, 0.000000000000000000 ) ) ;
#9795=ORIENTED_EDGE ( 'NONE', *, *, #12615, .F. ) ;
#9796=DIRECTION ( 'NONE',  ( -1.000000000000000000, 0.000000000000000000, -0.000000000000000000 ) ) ;
#9799=DIRECTION ( 'NONE',  ( 0.000000000000000000, 0.000000000000000000, 1.000000000000000000 ) ) ;
#9805=ORIENTED_EDGE ( 'NONE', *, *, #15415, .T. ) ;
#9820=EDGE_CURVE ( 'NONE', #890, #808, #8499, .T. ) ;
#9828=AXIS2_PLACEMENT_3D ( 'NONE', #5337, #8491, #9730 ) ;
#9838=ORIENTED_EDGE ( 'NONE', *, *, #7118, .T. ) ;
#9839=DIRECTION ( 'NONE',  ( 0.000000000000000000, 0.000000000000000000, 1.000000000000000000 ) ) ;
#9842=AXIS2_PLACEMENT_3D ( 'NONE', #517, #10695, #18123 ) ;
#9850=ADVANCED_FACE ( 'NONE', ( #9919 ), #15737, .T. ) ;
#9853=DIRECTION ( 'NONE',  ( -1.000000000000000000, -0.000000000000000000, -0.000000000000000000 ) ) ;
#9857=CARTESIAN_POINT ( 'NONE',  ( 10.00000000000000000, -20.32630374611196800, 16.60877409751161693 ) ) ;
#9858=VERTEX_POINT ( 'NONE', #1355 ) ;
#9862=EDGE_LOOP ( 'NONE', ( #6836, #11382, #11230, #18737 ) ) ;
#9882=EDGE_CURVE ( 'NONE', #15207, #7869, #1625, .T. ) ;
#9884=FACE_OUTER_BOUND ( 'NONE', #10646, .T. ) ;
#9885=ORIENTED_EDGE ( 'NONE', *, *, #11861, .F. ) ;
#9886=VERTEX_POINT ( 'NONE', #17535 ) ;
#9892=VERTEX_POINT ( 'NONE', #1550 ) ;
#9898=CARTESIAN_POINT ( 'NONE',  ( 0.000000000000000000, 0.000000000000000000, 0.000000000000000000 ) ) ;
#9901=DIRECTION ( 'NONE',  ( 0.000000000000000000, 0.000000000000000000, -1.000000000000000000 ) ) ;
#9917=DIRECTION ( 'NONE',  ( 0.000000000000000000, 0.000000000000000000, 1.000000000000000000 ) ) ;
#9919=FACE_OUTER_BOUND ( 'NONE', #2545, .T. ) ;
#9930=AXIS2_PLACEMENT_3D ( 'NONE', #2571, #17160, #15538 ) ;
#9934=DIRECTION ( 'NONE',  ( 1.000000000000000000, 0.000000000000000000, 0.000000000000000000 ) ) ;
#9936=ORIENTED_EDGE ( 'NONE', *, *, #18405, .F. ) ;
#9947=EDGE_CURVE ( 'NONE', #7125, #13289, #8543, .T. ) ;
#9948=DIRECTION ( 'NONE',  ( -1.000000000000000000, -0.000000000000000000, -0.000000000000000000 ) ) ;
#9950=CIRCLE ( 'NONE', #12065, 12.00000000001200462 ) ;
#9965=DIRECTION ( 'NONE',  ( 0.000000000000000000, 0.000000000000000000, 1.000000000000000000 ) ) ;
#9968=CIRCLE ( 'NONE', #18803, 5.000000000000000000 ) ;
#9969=DIRECTION ( 'NONE',  ( 0.000000000000000000, -0.8090169943749530024, 0.5877852522924653655 ) ) ;
#9972=VECTOR ( 'NONE', #16325, 1000.000000000000000 ) ;
#9990=AXIS2_PLACEMENT_3D ( 'NONE', #13921, #887, #6684 ) ;
#10002=AXIS2_PLACEMENT_3D ( 'NONE', #5904, #6091, #14667 ) ;
#10010=FACE_OUTER_BOUND ( 'NONE', #1406, .T. ) ;
#10012=CYLINDRICAL_SURFACE ( 'NONE', #8771, 26.24900000002624978 ) ;
#10016=ADVANCED_FACE ( 'NONE', ( #12545 ), #18261, .T. ) ;
#10017=AXIS2_PLACEMENT_3D ( 'NONE', #3904, #18568, #1045 ) ;
#10019=VERTEX_POINT ( 'NONE', #12095 ) ;
#10020=ADVANCED_FACE ( 'NONE', ( #6286 ), #11989, .T. ) ;
#10027=CARTESIAN_POINT ( 'NONE',  ( 0.000000000000000000, 14.27431201565567243, -29.75305054077457356 ) ) ;
#10029=ORIENTED_EDGE ( 'NONE', *, *, #14958, .T. ) ;
#10033=VECTOR ( 'NONE', #7852, 1000.000000000000000 ) ;
#10036=EDGE_CURVE ( 'NONE', #7525, #941, #6187, .T. ) ;
#10041=CIRCLE ( 'NONE', #4269, 12.00000000001200284 ) ;
#10046=DIRECTION ( 'NONE',  ( 0.000000000000000000, 0.9510565162951523099, 0.3090169943749516701 ) ) ;
#10062=ORIENTED_EDGE ( 'NONE', *, *, #3537, .F. ) ;
#10065=DIRECTION ( 'NONE',  ( 0.000000000000000000, -0.9510565162951502005, -0.3090169943749581649 ) ) ;
#10067=CARTESIAN_POINT ( 'NONE',  ( 10.00000000000000000, 0.000000000000000000, 0.000000000000000000 ) ) ;
#10068=VECTOR ( 'NONE', #17038, 1000.000000000000000 ) ;
#10074=VERTEX_POINT ( 'NONE', #9046 ) ;
#10080=CARTESIAN_POINT ( 'NONE',  ( -10.00000000000000000, 0.000000000000000000, 0.000000000000000000 ) ) ;
#10082=LINE ( 'NONE', #4188, #8791 ) ;
#10086=CARTESIAN_POINT ( 'NONE',  ( -10.00000000000000000, 0.000000000000000000, 0.000000000000000000 ) ) ;
#10087=AXIS2_PLACEMENT_3D ( 'NONE', #9513, #16762, #15518 ) ;
#10091=CARTESIAN_POINT ( 'NONE',  ( 10.00000000000000000, -13.40641754777648487, -24.79895094899273644 ) ) ;
#10092=CARTESIAN_POINT ( 'NONE',  ( -10.00000000000000000, 0.000000000000000000, 0.000000000000000000 ) ) ;
#10098=CARTESIAN_POINT ( 'NONE',  ( 0.000000000000000000, 32.70783759231086663, -4.381479206523104963 ) ) ;
#10104=VERTEX_POINT ( 'NONE', #382 ) ;
#10105=DIRECTION ( 'NONE',  ( 0.000000000000000000, 0.000000000000000000, 1.000000000000000000 ) ) ;
#10126=DIRECTION ( 'NONE',  ( -1.000000000000000000, -0.000000000000000000, -0.000000000000000000 ) ) ;
#10133=DIRECTION ( 'NONE',  ( -1.000000000000000000, -0.000000000000000000, 0.000000000000000000 ) ) ;
#10135=DIRECTION ( 'NONE',  ( 0.000000000000000000, 0.000000000000000000, 1.000000000000000000 ) ) ;
#10144=VERTEX_POINT ( 'NONE', #14433 ) ;
#10151=LINE ( 'NONE', #1394, #4193 ) ;
#10152=EDGE_CURVE ( 'NONE', #6992, #16256, #13022, .T. ) ;
#10153=ORIENTED_EDGE ( 'NONE', *, *, #4456, .T. ) ;
#10155=CARTESIAN_POINT ( 'NONE',  ( 10.00000000000000000, -13.40641754777683126, 24.79895094899255170 ) ) ;
#10170=EDGE_CURVE ( 'NONE', #944, #17607, #10669, .T. ) ;
#10172=DIRECTION ( 'NONE',  ( 0.000000000000000000, 0.000000000000000000, 1.000000000000000000 ) ) ;
#10182=DIRECTION ( 'NONE',  ( 0.000000000000000000, 0.000000000000000000, 1.000000000000000000 ) ) ;
#10187=EDGE_CURVE ( 'NONE', #1965, #13213, #5784, .T. ) ;
#10188=DIRECTION ( 'NONE',  ( -1.000000000000000000, 0.000000000000000000, 0.000000000000000000 ) ) ;
#10192=CARTESIAN_POINT ( 'NONE',  ( 0.000000000000000000, 1.489278925039883239, -26.20671763660627107 ) ) ;
#10193=CIRCLE ( 'NONE', #8061, 33.00000000003299760 ) ;
#10205=DIRECTION ( 'NONE',  ( -1.000000000000000000, 0.000000000000000000, 0.000000000000000000 ) ) ;
#10207=ORIENTED_EDGE ( 'NONE', *, *, #10985, .F. ) ;
#10211=DIRECTION ( 'NONE',  ( -0.000000000000000000, 0.000000000000000000, 1.000000000000000000 ) ) ;
#10217=ORIENTED_EDGE ( 'NONE', *, *, #10960, .F. ) ;
#10220=EDGE_CURVE ( 'NONE', #3486, #9332, #3694, .T. ) ;
#10222=DIRECTION ( 'NONE',  ( 0.000000000000000000, 0.000000000000000000, 1.000000000000000000 ) ) ;
#10227=CARTESIAN_POINT ( 'NONE',  ( 10.00000000000000000, -20.41355805489629915, 19.44239304137368407 ) ) ;
#10230=LINE ( 'NONE', #9857, #873 ) ;
#10232=ORIENTED_EDGE ( 'NONE', *, *, #2383, .F. ) ;
#10233=FACE_OUTER_BOUND ( 'NONE', #9862, .T. ) ;
#10242=AXIS2_PLACEMENT_3D ( 'NONE', #8757, #4209, #10377 ) ;
#10247=LINE ( 'NONE', #14719, #18472 ) ;
#10248=ORIENTED_EDGE ( 'NONE', *, *, #3129, .F. ) ;
#10251=ORIENTED_EDGE ( 'NONE', *, *, #4251, .T. ) ;
#10262=LINE ( 'NONE', #1323, #8079 ) ;
#10271=VECTOR ( 'NONE', #4314, 1000.000000000000000 ) ;
#10283=CIRCLE ( 'NONE', #12718, 12.00000000001200640 ) ;
#10288=ORIENTED_EDGE ( 'NONE', *, *, #6913, .T. ) ;
#10292=AXIS2_PLACEMENT_3D ( 'NONE', #15993, #3050, #9901 ) ;
#10293=EDGE_CURVE ( 'NONE', #11990, #17080, #5204, .T. ) ;
#10296=AXIS2_PLACEMENT_3D ( 'NONE', #16889, #5358, #12411 ) ;
#10301=DIRECTION ( 'NONE',  ( -1.000000000000000000, 0.000000000000000000, 0.000000000000000000 ) ) ;
#10302=STYLED_ITEM('',(#18890),#15847);
#10313=ORIENTED_EDGE ( 'NONE', *, *, #5959, .T. ) ;
#10321=ADVANCED_FACE ( 'NONE', ( #15013 ), #9101, .T. ) ;
#10322=CARTESIAN_POINT ( 'NONE',  ( 10.00000000000000000, 0.000000000000000000, 0.000000000000000000 ) ) ;
#10323=CYLINDRICAL_SURFACE ( 'NONE', #13111, 26.24900000002624978 ) ;
#10329=CARTESIAN_POINT ( 'NONE',  ( 10.00000000000000178, 6.799999999999999822, -1.500000000000000000 ) ) ;
#10332=DIRECTION ( 'NONE',  ( -1.000000000000000000, -0.000000000000000000, 0.000000000000000000 ) ) ;
#10340=AXIS2_PLACEMENT_3D ( 'NONE', #16048, #13190, #15950 ) ;
#10346=ORIENTED_EDGE ( 'NONE', *, *, #7272, .F. ) ;
#10356=EDGE_CURVE ( 'NONE', #205, #4486, #14336, .T. ) ;
#10365=EDGE_LOOP ( 'NONE', ( #4593, #11998, #3032, #7919, #10766, #11927 ) ) ;
#10366=CARTESIAN_POINT ( 'NONE',  ( 10.00000000000000000, 0.000000000000000000, 0.000000000000000000 ) ) ;
#10368=DIRECTION ( 'NONE',  ( 0.000000000000000000, -1.000000000000000000, -0.000000000000000000 ) ) ;
#10372=CARTESIAN_POINT ( 'NONE',  ( 0.000000000000000000, -14.27431201565546637, 29.75305054077467304 ) ) ;
#10377=DIRECTION ( 'NONE',  ( 0.000000000000000000, 0.000000000000000000, -1.000000000000000000 ) ) ;
#10385=ORIENTED_EDGE ( 'NONE', *, *, #2865, .T. ) ;
#10390=CIRCLE ( 'NONE', #18300, 26.24900000002624978 ) ;
#10397=CARTESIAN_POINT ( 'NONE',  ( 10.00000000000000000, -27.94286728106390072, -3.730438010304629515 ) ) ;
#10399=EDGE_CURVE ( 'NONE', #195, #18379, #6117, .T. ) ;
#10403=ORIENTED_EDGE ( 'NONE', *, *, #15326, .F. ) ;
#10405=EDGE_CURVE ( 'NONE', #14912, #9886, #17098, .T. ) ;
#10408=DIRECTION ( 'NONE',  ( -1.000000000000000000, 0.000000000000000000, 0.000000000000000000 ) ) ;
#10412=CARTESIAN_POINT ( 'NONE',  ( 0.000000000000000000, -27.72801475327278453, 6.913036516934497833 ) ) ;
#10413=DIRECTION ( 'NONE',  ( 0.000000000000000000, 0.8090169943749446757, 0.5877852522924769119 ) ) ;
#10414=FACE_OUTER_BOUND ( 'NONE', #18053, .T. ) ;
#10424=DIRECTION ( 'NONE',  ( -1.000000000000000000, -0.000000000000000000, 0.000000000000000000 ) ) ;
#10425=DIRECTION ( 'NONE',  ( -1.000000000000000000, -0.000000000000000000, -0.000000000000000000 ) ) ;
#10432=CARTESIAN_POINT ( 'NONE',  ( 0.000000000000000000, 13.40641754777700534, -24.79895094899245933 ) ) ;
#10441=CARTESIAN_POINT ( 'NONE',  ( 10.00000000000000000, -29.03656532225574693, 15.68049343255986017 ) ) ;
#10448=VERTEX_POINT ( 'NONE', #5093 ) ;
#10450=CYLINDRICAL_SURFACE ( 'NONE', #2575, 12.00000000001200107 ) ;
#10452=ORIENTED_EDGE ( 'NONE', *, *, #2482, .T. ) ;
#10455=DIRECTION ( 'NONE',  ( -1.000000000000000000, -0.000000000000000000, 0.000000000000000000 ) ) ;
#10458=ORIENTED_EDGE ( 'NONE', *, *, #5149, .T. ) ;
#10460=VERTEX_POINT ( 'NONE', #9663 ) ;
#10480=CARTESIAN_POINT ( 'NONE',  ( 50.00005079999999680, 0.000000000000000000, 1.500000000000000000 ) ) ;
#10490=ORIENTED_EDGE ( 'NONE', *, *, #13196, .T. ) ;
#10500=DIRECTION ( 'NONE',  ( -1.000000000000000000, 0.000000000000000000, 0.000000000000000000 ) ) ;
#10505=CARTESIAN_POINT ( 'NONE',  ( 0.000000000000000000, 0.000000000000000000, 0.000000000000000000 ) ) ;
#10507=CIRCLE ( 'NONE', #15977, 12.00000000001200817 ) ;
#10508=ORIENTED_EDGE ( 'NONE', *, *, #2375, .F. ) ;
#10515=EDGE_CURVE ( 'NONE', #10912, #15870, #7863, .T. ) ;
#10528=ORIENTED_EDGE ( 'NONE', *, *, #14289, .F. ) ;
#10532=DIRECTION ( 'NONE',  ( -1.000000000000000000, -0.000000000000000000, -0.000000000000000000 ) ) ;
#10533=DIRECTION ( 'NONE',  ( 0.000000000000000000, 0.000000000000000000, -1.000000000000000000 ) ) ;
#10534=AXIS2_PLACEMENT_3D ( 'NONE', #17850, #4803, #5941 ) ;
#10540=ORIENTED_EDGE ( 'NONE', *, *, #1904, .F. ) ;
#10548=VECTOR ( 'NONE', #13987, 1000.000000000000000 ) ;
#10550=VERTEX_POINT ( 'NONE', #2521 ) ;
#10560=VERTEX_POINT ( 'NONE', #12908 ) ;
#10572=CIRCLE ( 'NONE', #6002, 26.24900000002624978 ) ;
#10600=CIRCLE ( 'NONE', #1505, 12.00000000001200462 ) ;
#10621=EDGE_LOOP ( 'NONE', ( #6285, #11063, #10217, #4598 ) ) ;
#10624=CARTESIAN_POINT ( 'NONE',  ( 0.000000000000000000, 9.514709542737238124, -24.46385708179973406 ) ) ;
#10635=AXIS2_PLACEMENT_3D ( 'NONE', #446, #16741, #13503 ) ;
#10636=EDGE_CURVE ( 'NONE', #10019, #5831, #5664, .T. ) ;
#10645=AXIS2_PLACEMENT_3D ( 'NONE', #4410, #3173, #16037 ) ;
#10646=EDGE_LOOP ( 'NONE', ( #4613, #828, #14584, #83 ) ) ;
#10647=DIRECTION ( 'NONE',  ( -1.000000000000000000, -0.000000000000000000, 0.000000000000000000 ) ) ;
#10666=VERTEX_POINT ( 'NONE', #17194 ) ;
#10669=CIRCLE ( 'NONE', #4900, 26.24900000002626044 ) ;
#10670=CARTESIAN_POINT ( 'NONE',  ( 5.000000000000000000, -15.68049343256016570, 29.03656532225557996 ) ) ;
#10676=EDGE_LOOP ( 'NONE', ( #11780, #17781, #12552, #6690 ) ) ;
#10677=EDGE_CURVE ( 'NONE', #15251, #7427, #11868, .T. ) ;
#10678=EDGE_LOOP ( 'NONE', ( #10727, #13192, #1401, #4358 ) ) ;
#10681=CARTESIAN_POINT ( 'NONE',  ( 0.000000000000000000, 22.76987570971561681, -23.88582760061456511 ) ) ;
#10690=ORIENTED_EDGE ( 'NONE', *, *, #15810, .F. ) ;
#10695=DIRECTION ( 'NONE',  ( -1.000000000000000000, -0.000000000000000000, 0.000000000000000000 ) ) ;
#10697=ORIENTED_EDGE ( 'NONE', *, *, #13957, .F. ) ;
#10710=DIRECTION ( 'NONE',  ( 0.000000000000000000, 0.8090169943749445647, 0.5877852522924770229 ) ) ;
#10717=DIRECTION ( 'NONE',  ( 0.000000000000000000, 0.000000000000000000, 1.000000000000000000 ) ) ;
#10725=DIRECTION ( 'NONE',  ( 0.000000000000000000, 0.000000000000000000, 1.000000000000000000 ) ) ;
#10727=ORIENTED_EDGE ( 'NONE', *, *, #6803, .F. ) ;
#10736=EDGE_CURVE ( 'NONE', #3305, #18793, #4789, .T. ) ;
#10738=DIRECTION ( 'NONE',  ( 0.000000000000000000, 0.5877852522924742473, -0.8090169943749465631 ) ) ;
#10740=DIRECTION ( 'NONE',  ( -1.000000000000000000, 0.000000000000000000, -0.000000000000000000 ) ) ;
#10743=ORIENTED_EDGE ( 'NONE', *, *, #6450, .T. ) ;
#10746=LINE ( 'NONE', #667, #18347 ) ;
#10750=ORIENTED_EDGE ( 'NONE', *, *, #14958, .F. ) ;
#10752=ORIENTED_EDGE ( 'NONE', *, *, #9820, .T. ) ;
#10760=CARTESIAN_POINT ( 'NONE',  ( 0.000000000000000000, 27.72801475327282361, -5.086963483077305170 ) ) ;
#10766=ORIENTED_EDGE ( 'NONE', *, *, #4251, .F. ) ;
#10778=CARTESIAN_POINT ( 'NONE',  ( 10.00000000000000000, -22.07705612348828694, -14.19907017806892569 ) ) ;
#10779=VERTEX_POINT ( 'NONE', #14513 ) ;
#10791=CIRCLE ( 'NONE', #1074, 33.00000000003299760 ) ;
#10794=CARTESIAN_POINT ( 'NONE',  ( 0.000000000000000000, -3.730438010304518492, 27.94286728106391138 ) ) ;
#10798=ORIENTED_EDGE ( 'NONE', *, *, #15478, .T. ) ;
#10803=AXIS2_PLACEMENT_3D ( 'NONE', #17543, #14593, #1630 ) ;
#10807=ORIENTED_EDGE ( 'NONE', *, *, #3670, .T. ) ;
#10809=DIRECTION ( 'NONE',  ( 1.000000000000000000, 0.000000000000000000, 0.000000000000000000 ) ) ;
#10810=SHAPE_REPRESENTATION_RELATIONSHIP ( 'NONE' , 'NONE' ,  #13460, #6260 ) ;
#10822=DIRECTION ( 'NONE',  ( 0.000000000000000000, 0.000000000000000000, 1.000000000000000000 ) ) ;
#10828=AXIS2_PLACEMENT_3D ( 'NONE', #5823, #11549, #8674 ) ;
#10836=DIRECTION ( 'NONE',  ( -1.000000000000000000, 0.000000000000000000, 0.000000000000000000 ) ) ;
#10843=EDGE_CURVE ( 'NONE', #10448, #941, #621, .T. ) ;
#10844=ORIENTED_EDGE ( 'NONE', *, *, #5464, .F. ) ;
#10855=ADVANCED_FACE ( 'NONE', ( #901 ), #13742, .T. ) ;
#10867=ORIENTED_EDGE ( 'NONE', *, *, #13532, .T. ) ;
#10871=LINE ( 'NONE', #7829, #3983 ) ;
#10874=DIRECTION ( 'NONE',  ( 0.000000000000000000, 0.000000000000000000, 1.000000000000000000 ) ) ;
#10877=DIRECTION ( 'NONE',  ( -1.000000000000000000, -0.000000000000000000, -0.000000000000000000 ) ) ;
#10881=ORIENTED_EDGE ( 'NONE', *, *, #15065, .F. ) ;
#10882=ADVANCED_FACE ( 'NONE', ( #13826 ), #12300, .T. ) ;
#10896=FACE_OUTER_BOUND ( 'NONE', #7318, .T. ) ;
#10906=AXIS2_PLACEMENT_3D ( 'NONE', #7231, #13054, #10182 ) ;
#10907=DIRECTION ( 'NONE',  ( 0.000000000000000000, 0.000000000000000000, 1.000000000000000000 ) ) ;
#10908=ORIENTED_EDGE ( 'NONE', *, *, #1687, .F. ) ;
#10912=VERTEX_POINT ( 'NONE', #4967 ) ;
#10922=CIRCLE ( 'NONE', #16106, 12.00000000001200640 ) ;
#10926=DIRECTION ( 'NONE',  ( -1.000000000000000000, -0.000000000000000000, -0.000000000000000000 ) ) ;
#10935=FACE_OUTER_BOUND ( 'NONE', #9562, .T. ) ;
#10952=FACE_OUTER_BOUND ( 'NONE', #14471, .T. ) ;
#10955=ORIENTED_EDGE ( 'NONE', *, *, #12584, .F. ) ;
#10957=VERTEX_POINT ( 'NONE', #9165 ) ;
#10960=EDGE_CURVE ( 'NONE', #14062, #7869, #13578, .T. ) ;
#10963=LINE ( 'NONE', #16878, #15418 ) ;
#10965=FACE_OUTER_BOUND ( 'NONE', #16350, .T. ) ;
#10967=CARTESIAN_POINT ( 'NONE',  ( 10.00000000000000000, 3.730438010304324425, 27.94286728106393980 ) ) ;
#10973=LINE ( 'NONE', #14225, #2090 ) ;
#10985=EDGE_CURVE ( 'NONE', #7427, #10989, #1358, .T. ) ;
#10986=DIRECTION ( 'NONE',  ( 0.000000000000000000, 0.000000000000000000, 1.000000000000000000 ) ) ;
#10989=VERTEX_POINT ( 'NONE', #5554 ) ;
#10995=VECTOR ( 'NONE', #12303, 1000.000000000000000 ) ;
#11009=ORIENTED_EDGE ( 'NONE', *, *, #13363, .T. ) ;
#11012=CARTESIAN_POINT ( 'NONE',  ( 0.000000000000000000, 0.000000000000000000, 0.000000000000000000 ) ) ;
#11016=VERTEX_POINT ( 'NONE', #4036 ) ;
#11032=ORIENTED_EDGE ( 'NONE', *, *, #16874, .F. ) ;
#11034=CIRCLE ( 'NONE', #15303, 12.00000000001200462 ) ;
#11036=CARTESIAN_POINT ( 'NONE',  ( 10.00000000000000000, 4.381479206523443359, -32.70783759231081689 ) ) ;
#11053=DIRECTION ( 'NONE',  ( -1.000000000000000000, -0.000000000000000000, 0.000000000000000000 ) ) ;
#11062=DIRECTION ( 'NONE',  ( -1.000000000000000000, -0.000000000000000000, 0.000000000000000000 ) ) ;
#11063=ORIENTED_EDGE ( 'NONE', *, *, #9882, .T. ) ;
#11069=DIRECTION ( 'NONE',  ( -1.000000000000000000, -0.000000000000000000, 0.000000000000000000 ) ) ;
#11074=( GEOMETRIC_REPRESENTATION_CONTEXT ( 3 ) GLOBAL_UNCERTAINTY_ASSIGNED_CONTEXT ( ( #9785 ) ) GLOBAL_UNIT_ASSIGNED_CONTEXT ( ( #85, #3036, #3122 ) ) REPRESENTATION_CONTEXT ( 'NONE', 'WORKASPACE' ) );
#11088=DIRECTION ( 'NONE',  ( -1.000000000000000000, 0.000000000000000000, -0.000000000000000000 ) ) ;
#11102=CIRCLE ( 'NONE', #1985, 26.24900000002624978 ) ;
#11109=ORIENTED_EDGE ( 'NONE', *, *, #53, .F. ) ;
#11118=AXIS2_PLACEMENT_3D ( 'NONE', #16633, #18343, #6638 ) ;
#11127=AXIS2_PLACEMENT_3D ( 'NONE', #15473, #11069, #9370 ) ;
#11144=DIRECTION ( 'NONE',  ( 0.000000000000000000, -1.000000000000000000, -1.040834085585042960E-14 ) ) ;
#11147=AXIS2_PLACEMENT_3D ( 'NONE', #7897, #12273, #15142 ) ;
#11148=AXIS2_PLACEMENT_3D ( 'NONE', #5325, #5441, #17069 ) ;
#11154=ORIENTED_EDGE ( 'NONE', *, *, #2608, .T. ) ;
#11155=DIRECTION ( 'NONE',  ( -1.000000000000000000, 0.000000000000000000, 0.000000000000000000 ) ) ;
#11165=ORIENTED_EDGE ( 'NONE', *, *, #1801, .T. ) ;
#11177=CARTESIAN_POINT ( 'NONE',  ( 10.00000000000000000, 24.46385708179996854, -9.514709542736643044 ) ) ;
#11185=CARTESIAN_POINT ( 'NONE',  ( 10.00000000000000000, 6.681932690256967788, 25.38428207620324883 ) ) ;
#11193=CARTESIAN_POINT ( 'NONE',  ( 10.00000000000000000, 0.000000000000000000, 0.000000000000000000 ) ) ;
#11197=VERTEX_POINT ( 'NONE', #1627 ) ;
#11198=CIRCLE ( 'NONE', #13637, 26.24900000002624978 ) ;
#11203=DIRECTION ( 'NONE',  ( -1.000000000000000000, -0.000000000000000000, -0.000000000000000000 ) ) ;
#11206=DIRECTION ( 'NONE',  ( 0.000000000000000000, -0.8090169943749532244, 0.5877852522924652545 ) ) ;
#11207=AXIS2_PLACEMENT_3D ( 'NONE', #984, #6873, #3652 ) ;
#11208=VECTOR ( 'NONE', #6834, 1000.000000000000000 ) ;
#11210=EDGE_CURVE ( 'NONE', #7022, #15970, #7625, .T. ) ;
#11212=ADVANCED_FACE ( 'NONE', ( #5826 ), #14676, .T. ) ;
#11217=CARTESIAN_POINT ( 'NONE',  ( 10.00000000000000000, -6.681932690257146312, 25.38428207620320620 ) ) ;
#11230=ORIENTED_EDGE ( 'NONE', *, *, #12997, .T. ) ;
#11239=ORIENTED_EDGE ( 'NONE', *, *, #8452, .F. ) ;
#11242=LINE ( 'NONE', #11421, #4760 ) ;
#11245=CARTESIAN_POINT ( 'NONE',  ( 5.000000000000000000, -32.46095361140696411, 5.940243314904090077 ) ) ;
#11248=CARTESIAN_POINT ( 'NONE',  ( 10.00000000000000000, 5.086963483077203918, 27.72801475327284138 ) ) ;
#11255=AXIS2_PLACEMENT_3D ( 'NONE', #17197, #17739, #10222 ) ;
#11257=VERTEX_POINT ( 'NONE', #5911 ) ;
#11259=CARTESIAN_POINT ( 'NONE',  ( 10.00000000000000000, 14.19907017806900207, -22.07705612348824076 ) ) ;
#11265=CYLINDRICAL_SURFACE ( 'NONE', #3266, 33.00000000003299760 ) ;
#11275=ORIENTED_EDGE ( 'NONE', *, *, #16440, .F. ) ;
#11283=CARTESIAN_POINT ( 'NONE',  ( 10.00000000000000000, 22.07705612348859958, -14.19907017806844252 ) ) ;
#11285=EDGE_CURVE ( 'NONE', #38, #5250, #3257, .T. ) ;
#11286=CARTESIAN_POINT ( 'NONE',  ( 0.000000000000000000, 20.41355805489643060, -19.44239304137353841 ) ) ;
#11298=CARTESIAN_POINT ( 'NONE',  ( 10.00000000000000000, 27.94286728106398243, -3.730438010304017116 ) ) ;
#11306=DIRECTION ( 'NONE',  ( -1.000000000000000000, 0.000000000000000000, 0.000000000000000000 ) ) ;
#11314=ORIENTED_EDGE ( 'NONE', *, *, #9820, .F. ) ;
#11316=DIRECTION ( 'NONE',  ( 0.000000000000000000, 0.000000000000000000, 1.000000000000000000 ) ) ;
#11324=EDGE_CURVE ( 'NONE', #17432, #4065, #7193, .T. ) ;
#11328=VERTEX_POINT ( 'NONE', #11992 ) ;
#11331=CARTESIAN_POINT ( 'NONE',  ( 0.000000000000000000, 0.000000000000000000, 0.000000000000000000 ) ) ;
#11337=VECTOR ( 'NONE', #6411, 1000.000000000000000 ) ;
#11363=PLANE ( 'NONE',  #4389 ) ;
#11380=CARTESIAN_POINT ( 'NONE',  ( -10.00000000000000000, 0.000000000000000000, 0.000000000000000000 ) ) ;
#11381=ORIENTED_EDGE ( 'NONE', *, *, #13995, .T. ) ;
#11382=ORIENTED_EDGE ( 'NONE', *, *, #15050, .T. ) ;
#11387=ORIENTED_EDGE ( 'NONE', *, *, #14210, .T. ) ;
#11391=CARTESIAN_POINT ( 'NONE',  ( 10.00000000000000000, -3.730438010304114371, -27.94286728106396822 ) ) ;
#11395=DIRECTION ( 'NONE',  ( -1.000000000000000000, 0.000000000000000000, 0.000000000000000000 ) ) ;
#11396=DIRECTION ( 'NONE',  ( -1.000000000000000000, 0.000000000000000000, 0.000000000000000000 ) ) ;
#11398=ORIENTED_EDGE ( 'NONE', *, *, #5658, .F. ) ;
#11399=DIRECTION ( 'NONE',  ( -1.000000000000000000, 0.000000000000000000, 0.000000000000000000 ) ) ;
#11400=ORIENTED_EDGE ( 'NONE', *, *, #13897, .T. ) ;
#11401=CARTESIAN_POINT ( 'NONE',  ( 10.00000000000000000, 0.000000000000000000, 0.000000000000000000 ) ) ;
#11403=ORIENTED_EDGE ( 'NONE', *, *, #15143, .T. ) ;
#11404=ORIENTED_EDGE ( 'NONE', *, *, #198, .T. ) ;
#11408=ORIENTED_EDGE ( 'NONE', *, *, #4101, .F. ) ;
#11413=AXIS2_PLACEMENT_3D ( 'NONE', #11969, #17778, #10725 ) ;
#11416=ORIENTED_EDGE ( 'NONE', *, *, #7274, .F. ) ;
#11421=CARTESIAN_POINT ( 'NONE',  ( 10.00000000000000000, 20.32630374611208879, -16.60877409751146416 ) ) ;
#11429=ORIENTED_EDGE ( 'NONE', *, *, #13528, .F. ) ;
#11430=CARTESIAN_POINT ( 'NONE',  ( 0.000000000000000000, 0.000000000000000000, 0.000000000000000000 ) ) ;
#11435=EDGE_LOOP ( 'NONE', ( #7686, #925, #17496, #12400 ) ) ;
#11436=ORIENTED_EDGE ( 'NONE', *, *, #13957, .T. ) ;
#11444=FACE_OUTER_BOUND ( 'NONE', #1128, .T. ) ;
#11463=CARTESIAN_POINT ( 'NONE',  ( 0.000000000000000000, 0.000000000000000000, 0.000000000000000000 ) ) ;
#11470=ORIENTED_EDGE ( 'NONE', *, *, #11665, .F. ) ;
#11471=EDGE_CURVE ( 'NONE', #2470, #890, #5695, .T. ) ;
#11479=CARTESIAN_POINT ( 'NONE',  ( 10.00000000000000000, -20.41355805489629915, 19.44239304137368407 ) ) ;
#11482=CARTESIAN_POINT ( 'NONE',  ( 0.000000000000000000, 12.18267823974788122, -25.42247726998001411 ) ) ;
#11484=DIRECTION ( 'NONE',  ( 0.000000000000000000, -0.9510565162951565288, 0.3090169943749382919 ) ) ;
#11487=CIRCLE ( 'NONE', #14506, 26.24900000002625333 ) ;
#11499=DIRECTION ( 'NONE',  ( -1.000000000000000000, -0.000000000000000000, 0.000000000000000000 ) ) ;
#11510=DIRECTION ( 'NONE',  ( -1.000000000000000000, -0.000000000000000000, -0.000000000000000000 ) ) ;
#11513=EDGE_LOOP ( 'NONE', ( #15606, #2667, #17668, #11789 ) ) ;
#11519=VECTOR ( 'NONE', #15770, 1000.000000000000000 ) ;
#11523=AXIS2_PLACEMENT_3D ( 'NONE', #8749, #1426, #11710 ) ;
#11526=ORIENTED_EDGE ( 'NONE', *, *, #6057, .T. ) ;
#11530=FACE_OUTER_BOUND ( 'NONE', #15218, .T. ) ;
#11542=DIRECTION ( 'NONE',  ( -1.000000000000000000, 0.000000000000000000, 0.000000000000000000 ) ) ;
#11544=DIRECTION ( 'NONE',  ( -1.000000000000000000, -0.000000000000000000, 0.000000000000000000 ) ) ;
#11545=CYLINDRICAL_SURFACE ( 'NONE', #18654, 5.000000000000000000 ) ;
#11547=VECTOR ( 'NONE', #13168, 1000.000000000000000 ) ;
#11549=DIRECTION ( 'NONE',  ( -1.000000000000000000, 0.000000000000000000, 0.000000000000000000 ) ) ;
#11554=CARTESIAN_POINT ( 'NONE',  ( 0.000000000000000000, 0.000000000000000000, -1.500000000000000000 ) ) ;
#11557=CARTESIAN_POINT ( 'NONE',  ( 10.00000000000000178, 0.000000000000000000, 0.000000000000000000 ) ) ;
#11559=CARTESIAN_POINT ( 'NONE',  ( 10.00000000000000000, 13.40641754777665717, 24.79895094899264052 ) ) ;
#11561=VECTOR ( 'NONE', #5498, 1000.000000000000000 ) ;
#11564=ORIENTED_EDGE ( 'NONE', *, *, #6845, .F. ) ;
#11566=EDGE_LOOP ( 'NONE', ( #6943, #5227, #3075, #14844 ) ) ;
#11570=AXIS2_PLACEMENT_3D ( 'NONE', #6274, #6726, #3425 ) ;
#11575=CARTESIAN_POINT ( 'NONE',  ( 0.000000000000000000, -25.38428207620317778, -6.681932690257235130 ) ) ;
#11597=DIRECTION ( 'NONE',  ( -1.000000000000000000, 0.000000000000000000, 0.000000000000000000 ) ) ;
#11601=ORIENTED_EDGE ( 'NONE', *, *, #14021, .F. ) ;
#11616=CARTESIAN_POINT ( 'NONE',  ( 10.00000000000000000, -20.32630374611172641, -16.60877409751190470 ) ) ;
#11621=CARTESIAN_POINT ( 'NONE',  ( 0.000000000000000000, 0.000000000000000000, 0.000000000000000000 ) ) ;
#11623=CARTESIAN_POINT ( 'NONE',  ( 50.00005079999999680, 4.769696007084728073, -1.500000000000000000 ) ) ;
#11626=DIRECTION ( 'NONE',  ( -1.000000000000000000, -0.000000000000000000, 0.000000000000000000 ) ) ;
#11632=ADVANCED_FACE ( 'NONE', ( #12951 ), #8748, .T. ) ;
#11637=ORIENTED_EDGE ( 'NONE', *, *, #5680, .T. ) ;
#11652=VERTEX_POINT ( 'NONE', #3049 ) ;
#11654=CIRCLE ( 'NONE', #9828, 12.00000000001200462 ) ;
#11655=DIRECTION ( 'NONE',  ( 0.000000000000000000, 0.000000000000000000, 1.000000000000000000 ) ) ;
#11657=CARTESIAN_POINT ( 'NONE',  ( 10.00000000000000178, 0.000000000000000000, 0.000000000000000000 ) ) ;
#11658=CARTESIAN_POINT ( 'NONE',  ( 10.00000000000000000, 0.000000000000000000, 0.000000000000000000 ) ) ;
#11665=EDGE_CURVE ( 'NONE', #14997, #923, #9334, .T. ) ;
#11669=ORIENTED_EDGE ( 'NONE', *, *, #976, .F. ) ;
#11678=DIRECTION ( 'NONE',  ( 0.000000000000000000, 0.000000000000000000, -1.000000000000000000 ) ) ;
#11682=DIRECTION ( 'NONE',  ( -1.000000000000000000, 0.000000000000000000, 0.000000000000000000 ) ) ;
#11683=ORIENTED_EDGE ( 'NONE', *, *, #6384, .T. ) ;
#11696=ORIENTED_EDGE ( 'NONE', *, *, #12039, .F. ) ;
#11700=ADVANCED_FACE ( 'NONE', ( #561 ), #13425, .T. ) ;
#11708=ORIENTED_EDGE ( 'NONE', *, *, #15415, .F. ) ;
#11709=DIRECTION ( 'NONE',  ( -1.000000000000000000, 0.000000000000000000, 0.000000000000000000 ) ) ;
#11710=DIRECTION ( 'NONE',  ( 0.000000000000000000, 0.000000000000000000, 1.000000000000000000 ) ) ;
#11714=CYLINDRICAL_SURFACE ( 'NONE', #7586, 12.00000000001200462 ) ;
#11715=DIRECTION ( 'NONE',  ( 0.000000000000000000, 0.000000000000000000, 1.000000000000000000 ) ) ;
#11717=LINE ( 'NONE', #8851, #16392 ) ;
#11722=ORIENTED_EDGE ( 'NONE', *, *, #5586, .T. ) ;
#11723=EDGE_CURVE ( 'NONE', #8620, #15269, #8413, .T. ) ;
#11725=CARTESIAN_POINT ( 'NONE',  ( 10.00000000000000000, 27.94286728106393269, 15.73043801031642808 ) ) ;
#11726=AXIS2_PLACEMENT_3D ( 'NONE', #8144, #18239, #6898 ) ;
#11727=ORIENTED_EDGE ( 'NONE', *, *, #9117, .T. ) ;
#11729=CARTESIAN_POINT ( 'NONE',  ( -10.00000000000000000, 0.000000000000000000, 0.000000000000000000 ) ) ;
#11732=FACE_OUTER_BOUND ( 'NONE', #2809, .T. ) ;
#11733=ORIENTED_EDGE ( 'NONE', *, *, #7387, .F. ) ;
#11734=CARTESIAN_POINT ( 'NONE',  ( 5.000000000000000000, -15.68049343255974826, -29.03656532225581088 ) ) ;
#11736=CARTESIAN_POINT ( 'NONE',  ( 0.000000000000000000, -32.70783759231089505, 4.381479206522877590 ) ) ;
#11746=DIRECTION ( 'NONE',  ( 0.000000000000000000, -1.000000000000000000, -1.040834085585042960E-14 ) ) ;
#11756=DIRECTION ( 'NONE',  ( 0.000000000000000000, 0.000000000000000000, 1.000000000000000000 ) ) ;
#11758=ADVANCED_FACE ( 'NONE', ( #9129 ), #2086, .T. ) ;
#11759=DIRECTION ( 'NONE',  ( 0.000000000000000000, 0.000000000000000000, 1.000000000000000000 ) ) ;
#11760=LINE ( 'NONE', #17386, #16525 ) ;
#11762=ORIENTED_EDGE ( 'NONE', *, *, #14370, .T. ) ;
#11780=ORIENTED_EDGE ( 'NONE', *, *, #8215, .F. ) ;
#11787=CIRCLE ( 'NONE', #5998, 5.000000000000000000 ) ;
#11789=ORIENTED_EDGE ( 'NONE', *, *, #18297, .T. ) ;
#11797=CIRCLE ( 'NONE', #18806, 5.000000000000000000 ) ;
#11798=ORIENTED_EDGE ( 'NONE', *, *, #7499, .T. ) ;
#11806=DIRECTION ( 'NONE',  ( 0.000000000000000000, 0.000000000000000000, 1.000000000000000000 ) ) ;
#11807=CARTESIAN_POINT ( 'NONE',  ( 10.00000000000000000, 22.07705612348840063, 14.19907017806876404 ) ) ;
#11810=VERTEX_POINT ( 'NONE', #12180 ) ;
#11813=AXIS2_PLACEMENT_3D ( 'NONE', #18008, #12200, #6770 ) ;
#11825=AXIS2_PLACEMENT_3D ( 'NONE', #11401, #11510, #6940 ) ;
#11831=CARTESIAN_POINT ( 'NONE',  ( 10.00000000000000000, 20.41355805489615705, 19.44239304137382973 ) ) ;
#11836=CIRCLE ( 'NONE', #14579, 12.00000000001200640 ) ;
#11844=EDGE_CURVE ( 'NONE', #16169, #14282, #18164, .T. ) ;
#11855=ORIENTED_EDGE ( 'NONE', *, *, #10515, .F. ) ;
#11856=LINE ( 'NONE', #147, #8407 ) ;
#11861=EDGE_CURVE ( 'NONE', #6419, #3486, #15412, .T. ) ;
#11868=CIRCLE ( 'NONE', #12789, 26.24900000002625688 ) ;
#11891=ORIENTED_EDGE ( 'NONE', *, *, #12267, .F. ) ;
#11894=AXIS2_PLACEMENT_3D ( 'NONE', #16247, #3203, #15375 ) ;
#11904=DIRECTION ( 'NONE',  ( -1.000000000000000000, 0.000000000000000000, 0.000000000000000000 ) ) ;
#11905=EDGE_CURVE ( 'NONE', #13289, #13886, #3268, .T. ) ;
#11907=DIRECTION ( 'NONE',  ( -1.000000000000000000, 0.000000000000000000, -0.000000000000000000 ) ) ;
#11910=CIRCLE ( 'NONE', #10087, 26.24900000002625333 ) ;
#11923=EDGE_CURVE ( 'NONE', #13117, #1965, #15428, .T. ) ;
#11924=ORIENTED_EDGE ( 'NONE', *, *, #15871, .F. ) ;
#11927=ORIENTED_EDGE ( 'NONE', *, *, #9683, .F. ) ;
#11930=DIRECTION ( 'NONE',  ( 0.000000000000000000, 0.000000000000000000, 1.000000000000000000 ) ) ;
#11933=DIRECTION ( 'NONE',  ( -1.000000000000000000, 0.000000000000000000, 0.000000000000000000 ) ) ;
#11964=ORIENTED_EDGE ( 'NONE', *, *, #17754, .F. ) ;
#11968=DIRECTION ( 'NONE',  ( -1.000000000000000000, -0.000000000000000000, 0.000000000000000000 ) ) ;
#11969=CARTESIAN_POINT ( 'NONE',  ( 10.00000000000000000, 0.000000000000000000, 0.000000000000000000 ) ) ;
#11972=CARTESIAN_POINT ( 'NONE',  ( 5.000000000000000000, -29.75305054077462330, -14.27431201565557117 ) ) ;
#11975=ADVANCED_FACE ( 'NONE', ( #9502 ), #15315, .T. ) ;
#11989=CYLINDRICAL_SURFACE ( 'NONE', #3383, 12.00000000001200817 ) ;
#11990=VERTEX_POINT ( 'NONE', #1134 ) ;
#11992=CARTESIAN_POINT ( 'NONE',  ( 10.00000000000000000, -23.88582760061464683, -22.76987570971553509 ) ) ;
#11998=ORIENTED_EDGE ( 'NONE', *, *, #12370, .F. ) ;
#12001=CIRCLE ( 'NONE', #6844, 12.00000000001200462 ) ;
#12003=EDGE_LOOP ( 'NONE', ( #14707, #1913, #9678, #8810 ) ) ;
#12005=AXIS2_PLACEMENT_3D ( 'NONE', #4936, #4561, #10738 ) ;
#12006=ORIENTED_EDGE ( 'NONE', *, *, #13995, .F. ) ;
#12008=CIRCLE ( 'NONE', #8963, 26.24900000002624978 ) ;
#12021=AXIS2_PLACEMENT_3D ( 'NONE', #15388, #8161, #3873 ) ;
#12025=CYLINDRICAL_SURFACE ( 'NONE', #17228, 12.00000000001200462 ) ;
#12026=FACE_OUTER_BOUND ( 'NONE', #10676, .T. ) ;
#12030=ORIENTED_EDGE ( 'NONE', *, *, #17418, .F. ) ;
#12039=EDGE_CURVE ( 'NONE', #10957, #514, #12008, .T. ) ;
#12044=CIRCLE ( 'NONE', #12363, 33.00000000003299760 ) ;
#12047=ORIENTED_EDGE ( 'NONE', *, *, #13378, .F. ) ;
#12065=AXIS2_PLACEMENT_3D ( 'NONE', #3531, #877, #16962 ) ;
#12068=VERTEX_POINT ( 'NONE', #13277 ) ;
#12091=AXIS2_PLACEMENT_3D ( 'NONE', #6007, #1544, #18689 ) ;
#12095=CARTESIAN_POINT ( 'NONE',  ( 10.00000000000000000, -14.19907017806883864, 22.07705612348834734 ) ) ;
#12097=DIRECTION ( 'NONE',  ( 0.000000000000000000, 0.000000000000000000, 1.000000000000000000 ) ) ;
#12102=DIRECTION ( 'NONE',  ( -1.000000000000000000, 0.000000000000000000, 0.000000000000000000 ) ) ;
#12110=AXIS2_PLACEMENT_3D ( 'NONE', #18144, #18335, #10907 ) ;
#12114=VECTOR ( 'NONE', #9413, 1000.000000000000000 ) ;
#12116=CARTESIAN_POINT ( 'NONE',  ( 0.000000000000000000, -13.40641754777648487, -24.79895094899273644 ) ) ;
#12117=DIRECTION ( 'NONE',  ( 0.000000000000000000, 0.000000000000000000, 1.000000000000000000 ) ) ;
#12118=CARTESIAN_POINT ( 'NONE',  ( 0.000000000000000000, -22.76987570971544272, 23.88582760061473209 ) ) ;
#12123=CYLINDRICAL_SURFACE ( 'NONE', #18015, 33.00000000003299760 ) ;
#12126=CARTESIAN_POINT ( 'NONE',  ( 10.00000000000000000, 24.46385708179984064, 9.514709542736980552 ) ) ;
#12127=VERTEX_POINT ( 'NONE', #4273 ) ;
#12134=ORIENTED_EDGE ( 'NONE', *, *, #7274, .T. ) ;
#12141=ADVANCED_FACE ( 'NONE', ( #10414 ), #13381, .T. ) ;
#12143=EDGE_CURVE ( 'NONE', #13712, #12930, #15186, .T. ) ;
#12148=DIRECTION ( 'NONE',  ( 0.000000000000000000, 0.8090169943749446757, 0.5877852522924769119 ) ) ;
#12151=DIRECTION ( 'NONE',  ( 0.000000000000000000, -0.3090169943749548342, 0.9510565162951511997 ) ) ;
#12154=CARTESIAN_POINT ( 'NONE',  ( 10.00000000000000000, 24.79895094899259789, -13.40641754777674421 ) ) ;
#12155=ORIENTED_EDGE ( 'NONE', *, *, #6534, .T. ) ;
#12156=FACE_OUTER_BOUND ( 'NONE', #8546, .T. ) ;
#12158=AXIS2_PLACEMENT_3D ( 'NONE', #12288, #7914, #12198 ) ;
#12161=EDGE_CURVE ( 'NONE', #12340, #3488, #10791, .T. ) ;
#12163=CIRCLE ( 'NONE', #17355, 33.00000000003299760 ) ;
#12175=ORIENTED_EDGE ( 'NONE', *, *, #53, .T. ) ;
#12180=CARTESIAN_POINT ( 'NONE',  ( 0.000000000000000000, 4.769696007084728073, 1.500000000000000000 ) ) ;
#12181=CARTESIAN_POINT ( 'NONE',  ( 10.00000000000000000, 25.42247726998032320, -12.18267823974723640 ) ) ;
#12184=ORIENTED_EDGE ( 'NONE', *, *, #1904, .T. ) ;
#12186=ORIENTED_EDGE ( 'NONE', *, *, #8076, .T. ) ;
#12194=CARTESIAN_POINT ( 'NONE',  ( 10.00000000000000000, -27.72801475327278453, -5.086963483077506787 ) ) ;
#12198=DIRECTION ( 'NONE',  ( 0.000000000000000000, -0.8090169943749531134, 0.5877852522924653655 ) ) ;
#12200=DIRECTION ( 'NONE',  ( -1.000000000000000000, 0.000000000000000000, 0.000000000000000000 ) ) ;
#12212=DIRECTION ( 'NONE',  ( 0.000000000000000000, 0.000000000000000000, 1.000000000000000000 ) ) ;
#12213=DIRECTION ( 'NONE',  ( 0.000000000000000000, 0.9510565162951544194, -0.3090169943749447312 ) ) ;
#12214=DIRECTION ( 'NONE',  ( -1.000000000000000000, 0.000000000000000000, -0.000000000000000000 ) ) ;
#12215=CARTESIAN_POINT ( 'NONE',  ( 10.00000000000000000, 12.18267823974751352, 25.42247726998019530 ) ) ;
#12225=ORIENTED_EDGE ( 'NONE', *, *, #16510, .F. ) ;
#12228=DIRECTION ( 'NONE',  ( -1.000000000000000000, 0.000000000000000000, 0.000000000000000000 ) ) ;
#12242=VERTEX_POINT ( 'NONE', #2414 ) ;
#12249=EDGE_LOOP ( 'NONE', ( #11239, #17264, #6101, #8064 ) ) ;
#12255=LINE ( 'NONE', #651, #2651 ) ;
#12263=DIRECTION ( 'NONE',  ( -1.000000000000000000, 0.000000000000000000, -0.000000000000000000 ) ) ;
#12265=CARTESIAN_POINT ( 'NONE',  ( 10.00000000000000000, -5.086963483077008519, -27.72801475327286980 ) ) ;
#12267=EDGE_CURVE ( 'NONE', #15559, #17515, #13830, .T. ) ;
#12273=DIRECTION ( 'NONE',  ( -1.000000000000000000, 0.000000000000000000, 0.000000000000000000 ) ) ;
#12274=ORIENTED_EDGE ( 'NONE', *, *, #1863, .T. ) ;
#12275=CARTESIAN_POINT ( 'NONE',  ( 10.00000000000000000, -14.27431201565505070, -29.75305054077486488 ) ) ;
#12285=LINE ( 'NONE', #10670, #4500 ) ;
#12288=CARTESIAN_POINT ( 'NONE',  ( 0.000000000000000000, 0.000000000000000000, 0.000000000000000000 ) ) ;
#12294=ORIENTED_EDGE ( 'NONE', *, *, #14586, .F. ) ;
#12299=AXIS2_PLACEMENT_3D ( 'NONE', #15226, #1227, #5413 ) ;
#12300=CYLINDRICAL_SURFACE ( 'NONE', #6884, 33.00000000003299760 ) ;
#12303=DIRECTION ( 'NONE',  ( -1.000000000000000000, 0.000000000000000000, 0.000000000000000000 ) ) ;
#12319=VECTOR ( 'NONE', #8229, 1000.000000000000000 ) ;
#12329=AXIS2_PLACEMENT_3D ( 'NONE', #7750, #16436, #3294 ) ;
#12330=ORIENTED_EDGE ( 'NONE', *, *, #8375, .F. ) ;
#12334=LINE ( 'NONE', #18147, #4750 ) ;
#12336=ORIENTED_EDGE ( 'NONE', *, *, #2704, .T. ) ;
#12338=LINE ( 'NONE', #2532, #12650 ) ;
#12340=VERTEX_POINT ( 'NONE', #14032 ) ;
#12343=CIRCLE ( 'NONE', #13577, 12.00000000001200462 ) ;
#12359=AXIS2_PLACEMENT_3D ( 'NONE', #408, #16220, #3171 ) ;
#12363=AXIS2_PLACEMENT_3D ( 'NONE', #13308, #16253, #13590 ) ;
#12365=VERTEX_POINT ( 'NONE', #4226 ) ;
#12370=EDGE_CURVE ( 'NONE', #18064, #1091, #3207, .T. ) ;
#12372=CIRCLE ( 'NONE', #8426, 12.00000000001200817 ) ;
#12374=ADVANCED_FACE ( 'NONE', ( #2789 ), #7158, .T. ) ;
#12378=ORIENTED_EDGE ( 'NONE', *, *, #18029, .T. ) ;
#12386=DIRECTION ( 'NONE',  ( 0.000000000000000000, 0.9510565162951543083, -0.3090169943749447867 ) ) ;
#12389=AXIS2_PLACEMENT_3D ( 'NONE', #12265, #7607, #1800 ) ;
#12398=CIRCLE ( 'NONE', #6341, 12.00000000001200640 ) ;
#12400=ORIENTED_EDGE ( 'NONE', *, *, #12161, .F. ) ;
#12406=DIRECTION ( 'NONE',  ( -1.000000000000000000, 0.000000000000000000, 0.000000000000000000 ) ) ;
#12409=CARTESIAN_POINT ( 'NONE',  ( 5.000000000000000000, -22.76987570971544272, 23.88582760061473209 ) ) ;
#12411=DIRECTION ( 'NONE',  ( 0.000000000000000000, 0.000000000000000000, 1.000000000000000000 ) ) ;
#12416=ORIENTED_EDGE ( 'NONE', *, *, #8759, .F. ) ;
#12427=DIRECTION ( 'NONE',  ( -1.000000000000000000, 0.000000000000000000, 0.000000000000000000 ) ) ;
#12428=CARTESIAN_POINT ( 'NONE',  ( 10.00000000000000000, -1.489278925039700052, 26.20671763660628173 ) ) ;
#12430=DIRECTION ( 'NONE',  ( 1.000000000000000000, -0.000000000000000000, -0.000000000000000000 ) ) ;
#12434=VECTOR ( 'NONE', #2950, 1000.000000000000000 ) ;
#12455=DIRECTION ( 'NONE',  ( -1.000000000000000000, 0.000000000000000000, 0.000000000000000000 ) ) ;
#12458=DIRECTION ( 'NONE',  ( -1.000000000000000000, -0.000000000000000000, -0.000000000000000000 ) ) ;
#12462=CARTESIAN_POINT ( 'NONE',  ( 0.000000000000000000, 0.000000000000000000, 0.000000000000000000 ) ) ;
#12485=ORIENTED_EDGE ( 'NONE', *, *, #6114, .F. ) ;
#12487=CARTESIAN_POINT ( 'NONE',  ( 10.00000000000000000, -4.381479206522757686, -32.70783759231090215 ) ) ;
#12514=ADVANCED_FACE ( 'NONE', ( #11732 ), #309, .T. ) ;
#12521=CARTESIAN_POINT ( 'NONE',  ( 10.00000000000000000, 0.000000000000000000, 0.000000000000000000 ) ) ;
#12538=DIRECTION ( 'NONE',  ( 0.000000000000000000, -0.5877852522924623679, -0.8090169943749552228 ) ) ;
#12545=FACE_OUTER_BOUND ( 'NONE', #1936, .T. ) ;
#12552=ORIENTED_EDGE ( 'NONE', *, *, #13378, .T. ) ;
#12558=CYLINDRICAL_SURFACE ( 'NONE', #17258, 12.00000000001200462 ) ;
#12562=CARTESIAN_POINT ( 'NONE',  ( 10.00000000000000000, 1.489278925039520418, 26.20671763660628883 ) ) ;
#12563=AXIS2_PLACEMENT_3D ( 'NONE', #14668, #5818, #17438 ) ;
#12564=EDGE_CURVE ( 'NONE', #14282, #1187, #7259, .T. ) ;
#12565=VERTEX_POINT ( 'NONE', #4498 ) ;
#12580=CARTESIAN_POINT ( 'NONE',  ( 0.000000000000000000, 6.681932690257323060, -25.38428207620315291 ) ) ;
#12584=EDGE_CURVE ( 'NONE', #6251, #12565, #4731, .T. ) ;
#12585=ORIENTED_EDGE ( 'NONE', *, *, #14641, .T. ) ;
#12596=DIRECTION ( 'NONE',  ( 0.000000000000000000, 0.000000000000000000, 1.000000000000000000 ) ) ;
#12597=EDGE_LOOP ( 'NONE', ( #10881, #18548, #2081, #7763 ) ) ;
#12599=CARTESIAN_POINT ( 'NONE',  ( -10.00000000000000000, 0.000000000000000000, 0.000000000000000000 ) ) ;
#12600=ORIENTED_EDGE ( 'NONE', *, *, #5533, .F. ) ;
#12601=ORIENTED_EDGE ( 'NONE', *, *, #14169, .F. ) ;
#12615=EDGE_CURVE ( 'NONE', #353, #10104, #14679, .T. ) ;
#12616=EDGE_CURVE ( 'NONE', #7427, #10448, #13570, .T. ) ;
#12625=AXIS2_PLACEMENT_3D ( 'NONE', #17988, #10740, #3511 ) ;
#12634=LINE ( 'NONE', #2347, #1970 ) ;
#12636=CARTESIAN_POINT ( 'NONE',  ( 10.00000000000000000, -24.46385708179976604, -9.514709542737152859 ) ) ;
#12644=CYLINDRICAL_SURFACE ( 'NONE', #1468, 12.00000000001200462 ) ;
#12650=VECTOR ( 'NONE', #2340, 1000.000000000000000 ) ;
#12654=DIRECTION ( 'NONE',  ( -1.000000000000000000, 0.000000000000000000, -0.000000000000000000 ) ) ;
#12702=DIRECTION ( 'NONE',  ( 0.000000000000000000, 1.000000000000000000, 3.469446951950143595E-15 ) ) ;
#12718=AXIS2_PLACEMENT_3D ( 'NONE', #11482, #7089, #17382 ) ;
#12726=CIRCLE ( 'NONE', #2065, 12.00000000001200640 ) ;
#12734=CARTESIAN_POINT ( 'NONE',  ( 10.00000000000000000, 12.18267823974788122, -25.42247726998001411 ) ) ;
#12737=VECTOR ( 'NONE', #10836, 1000.000000000000000 ) ;
#12744=ORIENTED_EDGE ( 'NONE', *, *, #15810, .T. ) ;
#12750=EDGE_CURVE ( 'NONE', #5171, #14997, #12959, .T. ) ;
#12767=VECTOR ( 'NONE', #5109, 1000.000000000000000 ) ;
#12770=LINE ( 'NONE', #5613, #12434 ) ;
#12771=DIRECTION ( 'NONE',  ( -1.000000000000000000, -0.000000000000000000, 0.000000000000000000 ) ) ;
#12781=CYLINDRICAL_SURFACE ( 'NONE', #14386, 12.00000000001200462 ) ;
#12789=AXIS2_PLACEMENT_3D ( 'NONE', #2614, #8433, #14243 ) ;
#12797=VERTEX_POINT ( 'NONE', #7911 ) ;
#12798=DIRECTION ( 'NONE',  ( -1.000000000000000000, -0.000000000000000000, -0.000000000000000000 ) ) ;
#12801=CARTESIAN_POINT ( 'NONE',  ( 0.000000000000000000, 0.000000000000000000, 0.000000000000000000 ) ) ;
#12807=ORIENTED_EDGE ( 'NONE', *, *, #2608, .F. ) ;
#12812=DIRECTION ( 'NONE',  ( -1.000000000000000000, -0.000000000000000000, -0.000000000000000000 ) ) ;
#12822=CYLINDRICAL_SURFACE ( 'NONE', #1821, 33.00000000003299760 ) ;
#12823=EDGE_LOOP ( 'NONE', ( #12336, #14118, #9757, #1153 ) ) ;
#12832=DIRECTION ( 'NONE',  ( -1.000000000000000000, 0.000000000000000000, -0.000000000000000000 ) ) ;
#12833=ORIENTED_EDGE ( 'NONE', *, *, #13325, .T. ) ;
#12856=EDGE_CURVE ( 'NONE', #10989, #12127, #16609, .T. ) ;
#12862=PRODUCT_DEFINITION_SHAPE ( 'NONE', 'NONE',  #18768 ) ;
#12869=DIRECTION ( 'NONE',  ( -1.000000000000000000, 0.000000000000000000, 0.000000000000000000 ) ) ;
#12877=DIRECTION ( 'NONE',  ( 0.000000000000000000, -1.000000000000000000, -1.047444401652940164E-14 ) ) ;
#12903=ORIENTED_EDGE ( 'NONE', *, *, #14715, .T. ) ;
#12908=CARTESIAN_POINT ( 'NONE',  ( 0.000000000000000000, -4.381479206522764791, -32.70783759231090926 ) ) ;
#12912=CARTESIAN_POINT ( 'NONE',  ( 0.000000000000000000, -20.41355805489629915, 19.44239304137368407 ) ) ;
#12919=ORIENTED_EDGE ( 'NONE', *, *, #4124, .F. ) ;
#12922=CARTESIAN_POINT ( 'NONE',  ( 0.000000000000000000, -15.68049343256016925, 29.03656532225557996 ) ) ;
#12924=ORIENTED_EDGE ( 'NONE', *, *, #13158, .F. ) ;
#12925=CARTESIAN_POINT ( 'NONE',  ( 5.000000000000000000, -29.03656532225551601, -15.68049343256028294 ) ) ;
#12929=AXIS2_PLACEMENT_3D ( 'NONE', #10091, #14460, #4008 ) ;
#12930=VERTEX_POINT ( 'NONE', #10098 ) ;
#12936=ORIENTED_EDGE ( 'NONE', *, *, #5402, .F. ) ;
#12943=AXIS2_PLACEMENT_3D ( 'NONE', #16230, #3179, #3277 ) ;
#12946=AXIS2_PLACEMENT_3D ( 'NONE', #4087, #14082, #7984 ) ;
#12951=FACE_OUTER_BOUND ( 'NONE', #958, .T. ) ;
#12959=CIRCLE ( 'NONE', #14765, 26.24900000002625333 ) ;
#12960=EDGE_CURVE ( 'NONE', #7869, #12340, #2618, .T. ) ;
#12961=EDGE_CURVE ( 'NONE', #1091, #5783, #4655, .T. ) ;
#12969=CIRCLE ( 'NONE', #12021, 12.00000000001200640 ) ;
#12980=CARTESIAN_POINT ( 'NONE',  ( 0.000000000000000000, 0.000000000000000000, 0.000000000000000000 ) ) ;
#12989=ORIENTED_EDGE ( 'NONE', *, *, #12584, .T. ) ;
#12997=EDGE_CURVE ( 'NONE', #5171, #17453, #7328, .T. ) ;
#12999=PLANE ( 'NONE',  #15996 ) ;
#13001=AXIS2_PLACEMENT_3D ( 'NONE', #4217, #17265, #1175 ) ;
#13002=AXIS2_PLACEMENT_3D ( 'NONE', #2356, #12458, #18353 ) ;
#13013=CARTESIAN_POINT ( 'NONE',  ( 10.00000000000000000, 0.000000000000000000, 1.500000000000000000 ) ) ;
#13022=LINE ( 'NONE', #12925, #10068 ) ;
#13032=DIRECTION ( 'NONE',  ( 0.000000000000000000, 0.000000000000000000, 1.000000000000000000 ) ) ;
#13048=DIRECTION ( 'NONE',  ( -1.000000000000000000, 0.000000000000000000, 0.000000000000000000 ) ) ;
#13054=DIRECTION ( 'NONE',  ( -1.000000000000000000, -0.000000000000000000, -0.000000000000000000 ) ) ;
#13062=FACE_OUTER_BOUND ( 'NONE', #18662, .T. ) ;
#13071=CARTESIAN_POINT ( 'NONE',  ( 0.000000000000000000, -19.44239304137390434, 20.41355805489607889 ) ) ;
#13072=ORIENTED_EDGE ( 'NONE', *, *, #15862, .F. ) ;
#13080=ORIENTED_EDGE ( 'NONE', *, *, #2247, .F. ) ;
#13083=AXIS2_PLACEMENT_3D ( 'NONE', #12734, #14154, #12538 ) ;
#13094=AXIS2_PLACEMENT_3D ( 'NONE', #3675, #17862, #12148 ) ;
#13107=DIRECTION ( 'NONE',  ( -1.000000000000000000, -0.000000000000000000, -0.000000000000000000 ) ) ;
#13111=AXIS2_PLACEMENT_3D ( 'NONE', #17656, #10408, #7552 ) ;
#13117=VERTEX_POINT ( 'NONE', #3618 ) ;
#13126=CARTESIAN_POINT ( 'NONE',  ( 10.00000000000000178, 6.123233995736766282E-16, -5.000000000000000000 ) ) ;
#13132=DIRECTION ( 'NONE',  ( 0.000000000000000000, 0.000000000000000000, 1.000000000000000000 ) ) ;
#13144=ADVANCED_FACE ( 'NONE', ( #15037 ), #15233, .T. ) ;
#13145=DIRECTION ( 'NONE',  ( 0.000000000000000000, 0.000000000000000000, 1.000000000000000000 ) ) ;
#13152=VERTEX_POINT ( 'NONE', #566 ) ;
#13154=FACE_OUTER_BOUND ( 'NONE', #8397, .T. ) ;
#13155=APPLICATION_CONTEXT ( 'automotive_design' ) ;
#13158=EDGE_CURVE ( 'NONE', #6241, #1304, #15057, .T. ) ;
#13168=DIRECTION ( 'NONE',  ( 1.000000000000000000, 0.000000000000000000, -0.000000000000000000 ) ) ;
#13181=CARTESIAN_POINT ( 'NONE',  ( 5.000000000000000000, 5.940243314904670946, -32.46095361140686464 ) ) ;
#13186=CARTESIAN_POINT ( 'NONE',  ( 0.000000000000000000, 16.60877409751168798, 20.32630374611190760 ) ) ;
#13189=CARTESIAN_POINT ( 'NONE',  ( 10.00000000000000000, -16.60877409751182654, 20.32630374611179391 ) ) ;
#13190=DIRECTION ( 'NONE',  ( -1.000000000000000000, 0.000000000000000000, 0.000000000000000000 ) ) ;
#13192=ORIENTED_EDGE ( 'NONE', *, *, #12997, .F. ) ;
#13196=EDGE_CURVE ( 'NONE', #5299, #11990, #2585, .T. ) ;
#13203=ORIENTED_EDGE ( 'NONE', *, *, #10187, .F. ) ;
#13210=COLOUR_RGB ( '',1.000000000000000000, 0.9490196078431372140, 0.9098039215686274384 ) ;
#13211=DIRECTION ( 'NONE',  ( -1.000000000000000000, 0.000000000000000000, 0.000000000000000000 ) ) ;
#13213=VERTEX_POINT ( 'NONE', #4347 ) ;
#13234=CARTESIAN_POINT ( 'NONE',  ( 10.00000000000000000, 14.19907017806868588, 22.07705612348844326 ) ) ;
#13236=DIRECTION ( 'NONE',  ( 0.000000000000000000, 0.3090169943749479509, -0.9510565162951533091 ) ) ;
#13237=ORIENTED_EDGE ( 'NONE', *, *, #6384, .F. ) ;
#13240=AXIS2_PLACEMENT_3D ( 'NONE', #7296, #17760, #11678 ) ;
#13253=CARTESIAN_POINT ( 'NONE',  ( 4.999999999999999112, 32.46095361140700675, -5.940243314903876026 ) ) ;
#13256=ORIENTED_EDGE ( 'NONE', *, *, #6811, .T. ) ;
#13257=EDGE_CURVE ( 'NONE', #8847, #14291, #775, .T. ) ;
#13264=ORIENTED_EDGE ( 'NONE', *, *, #14210, .F. ) ;
#13274=FACE_OUTER_BOUND ( 'NONE', #2441, .T. ) ;
#13277=CARTESIAN_POINT ( 'NONE',  ( 10.00000000000000000, 32.70783759231085952, 4.381479206523099634 ) ) ;
#13289=VERTEX_POINT ( 'NONE', #153 ) ;
#13297=CARTESIAN_POINT ( 'NONE',  ( 10.00000000000000000, -16.60877409751153522, -20.32630374611203194 ) ) ;
#13299=EDGE_CURVE ( 'NONE', #364, #7035, #1072, .T. ) ;
#13308=CARTESIAN_POINT ( 'NONE',  ( 0.000000000000000000, 0.000000000000000000, 0.000000000000000000 ) ) ;
#13325=EDGE_CURVE ( 'NONE', #262, #4831, #15368, .T. ) ;
#13329=DIRECTION ( 'NONE',  ( -1.000000000000000000, 0.000000000000000000, 0.000000000000000000 ) ) ;
#13331=ORIENTED_EDGE ( 'NONE', *, *, #12961, .T. ) ;
#13336=AXIS2_PLACEMENT_3D ( 'NONE', #9283, #539, #7582 ) ;
#13339=FACE_OUTER_BOUND ( 'NONE', #9055, .T. ) ;
#13344=DIRECTION ( 'NONE',  ( -1.000000000000000000, -0.000000000000000000, 0.000000000000000000 ) ) ;
#13353=CIRCLE ( 'NONE', #13960, 33.00000000003299760 ) ;
#13358=CYLINDRICAL_SURFACE ( 'NONE', #973, 33.00000000003299760 ) ;
#13360=ORIENTED_EDGE ( 'NONE', *, *, #18080, .F. ) ;
#13363=EDGE_CURVE ( 'NONE', #10074, #808, #10193, .T. ) ;
#13368=EDGE_LOOP ( 'NONE', ( #10908, #7921, #1232, #18583 ) ) ;
#13370=VERTEX_POINT ( 'NONE', #6255 ) ;
#13372=FACE_OUTER_BOUND ( 'NONE', #3751, .T. ) ;
#13374=AXIS2_PLACEMENT_3D ( 'NONE', #11248, #11542, #15911 ) ;
#13378=EDGE_CURVE ( 'NONE', #3895, #9120, #3204, .T. ) ;
#13381=CYLINDRICAL_SURFACE ( 'NONE', #12943, 12.00000000001200462 ) ;
#13382=LINE ( 'NONE', #6128, #3934 ) ;
#13385=CYLINDRICAL_SURFACE ( 'NONE', #1930, 26.24900000002624978 ) ;
#13386=CARTESIAN_POINT ( 'NONE',  ( 0.000000000000000000, 15.68049343255996675, 29.03656532225569009 ) ) ;
#13393=CIRCLE ( 'NONE', #15522, 26.24900000002624978 ) ;
#13396=CARTESIAN_POINT ( 'NONE',  ( 0.000000000000000000, -12.18267823974732522, -25.42247726998028057 ) ) ;
#13422=CARTESIAN_POINT ( 'NONE',  ( 10.00000000000000000, -29.75305054077461975, -14.27431201565556940 ) ) ;
#13425=CYLINDRICAL_SURFACE ( 'NONE', #12389, 12.00000000001200462 ) ;
#13428=DIRECTION ( 'NONE',  ( -1.000000000000000000, 0.000000000000000000, -0.000000000000000000 ) ) ;
#13434=CARTESIAN_POINT ( 'NONE',  ( 0.000000000000000000, 32.46095361140700675, -5.940243314903877803 ) ) ;
#13439=EDGE_CURVE ( 'NONE', #4430, #17584, #9582, .T. ) ;
#13440=EDGE_LOOP ( 'NONE', ( #14723, #11408, #10232, #3380 ) ) ;
#13446=CIRCLE ( 'NONE', #14956, 26.24900000002624978 ) ;
#13452=LINE ( 'NONE', #11734, #11547 ) ;
#13456=ORIENTED_EDGE ( 'NONE', *, *, #15532, .F. ) ;
#13460=SHAPE_REPRESENTATION ( 'spur gear_iso_ISO - Spur gear 3M 20T 20PA 10FW ---S20A75H50L10.0S1', ( #8017 ), #11074 ) ;
#13465=CARTESIAN_POINT ( 'NONE',  ( 10.00000000000000000, 0.000000000000000000, 0.000000000000000000 ) ) ;
#13472=FACE_OUTER_BOUND ( 'NONE', #13368, .T. ) ;
#13474=CIRCLE ( 'NONE', #1901, 12.00000000001200462 ) ;
#13476=FACE_OUTER_BOUND ( 'NONE', #3779, .T. ) ;
#13478=EDGE_LOOP ( 'NONE', ( #15360, #16670, #6459, #5183 ) ) ;
#13486=EDGE_CURVE ( 'NONE', #17410, #11328, #12634, .T. ) ;
#13489=AXIS2_PLACEMENT_3D ( 'NONE', #4944, #378, #3431 ) ;
#13495=EDGE_LOOP ( 'NONE', ( #400, #1399, #15937, #1636 ) ) ;
#13503=DIRECTION ( 'NONE',  ( 0.000000000000000000, 0.000000000000000000, 1.000000000000000000 ) ) ;
#13507=VECTOR ( 'NONE', #14598, 1000.000000000000000 ) ;
#13519=DIRECTION ( 'NONE',  ( 0.000000000000000000, -0.9510565162951564178, 0.3090169943749384585 ) ) ;
#13525=DIRECTION ( 'NONE',  ( 1.000000000000000000, -0.000000000000000000, -0.000000000000000000 ) ) ;
#13528=EDGE_CURVE ( 'NONE', #17453, #13370, #10507, .T. ) ;
#13532=EDGE_CURVE ( 'NONE', #15320, #5321, #8086, .T. ) ;
#13534=DIRECTION ( 'NONE',  ( -1.000000000000000000, -0.000000000000000000, -0.000000000000000000 ) ) ;
#13539=CIRCLE ( 'NONE', #5318, 26.24900000002624978 ) ;
#13547=DIRECTION ( 'NONE',  ( -1.000000000000000000, 0.000000000000000000, 0.000000000000000000 ) ) ;
#13552=DIRECTION ( 'NONE',  ( -1.000000000000000000, -0.000000000000000000, 0.000000000000000000 ) ) ;
#13562=VERTEX_POINT ( 'NONE', #1392 ) ;
#13570=CIRCLE ( 'NONE', #15380, 12.00000000001200640 ) ;
#13576=CIRCLE ( 'NONE', #10534, 26.24900000002624978 ) ;
#13577=AXIS2_PLACEMENT_3D ( 'NONE', #17569, #10332, #7459 ) ;
#13578=CIRCLE ( 'NONE', #816, 12.00000000001200817 ) ;
#13587=ORIENTED_EDGE ( 'NONE', *, *, #16440, .T. ) ;
#13590=DIRECTION ( 'NONE',  ( 0.000000000000000000, 0.000000000000000000, 1.000000000000000000 ) ) ;
#13592=VECTOR ( 'NONE', #10647, 1000.000000000000000 ) ;
#13599=CYLINDRICAL_SURFACE ( 'NONE', #10635, 33.00000000003299760 ) ;
#13603=AXIS2_PLACEMENT_3D ( 'NONE', #10366, #8838, #14653 ) ;
#13608=EDGE_LOOP ( 'NONE', ( #9516, #5645, #61, #15527 ) ) ;
#13620=DIRECTION ( 'NONE',  ( -1.000000000000000000, 0.000000000000000000, 0.000000000000000000 ) ) ;
#13623=CARTESIAN_POINT ( 'NONE',  ( 0.000000000000000000, 26.20671763660628528, 1.489278925039608570 ) ) ;
#13630=VERTEX_POINT ( 'NONE', #5781 ) ;
#13633=FACE_OUTER_BOUND ( 'NONE', #4998, .T. ) ;
#13637=AXIS2_PLACEMENT_3D ( 'NONE', #2955, #100, #14381 ) ;
#13642=EDGE_LOOP ( 'NONE', ( #3424, #17605, #3791, #13940 ) ) ;
#13645=CIRCLE ( 'NONE', #3621, 12.00000000001200817 ) ;
#13647=ORIENTED_EDGE ( 'NONE', *, *, #3039, .F. ) ;
#13648=CIRCLE ( 'NONE', #9387, 12.00000000001200284 ) ;
#13650=ORIENTED_EDGE ( 'NONE', *, *, #2708, .T. ) ;
#13675=EDGE_CURVE ( 'NONE', #18365, #7876, #7295, .T. ) ;
#13694=SURFACE_SIDE_STYLE ('',( #5106 ) ) ;
#13703=VERTEX_POINT ( 'NONE', #12922 ) ;
#13707=ORIENTED_EDGE ( 'NONE', *, *, #5525, .F. ) ;
#13708=DIRECTION ( 'NONE',  ( -1.000000000000000000, 0.000000000000000000, 0.000000000000000000 ) ) ;
#13710=LINE ( 'NONE', #7690, #3733 ) ;
#13712=VERTEX_POINT ( 'NONE', #4264 ) ;
#13741=DIRECTION ( 'NONE',  ( -1.000000000000000000, -0.000000000000000000, -0.000000000000000000 ) ) ;
#13742=CYLINDRICAL_SURFACE ( 'NONE', #16008, 26.24900000002624978 ) ;
#13780=CIRCLE ( 'NONE', #7688, 33.00000000003299760 ) ;
#13786=DIRECTION ( 'NONE',  ( 0.000000000000000000, 0.000000000000000000, -1.000000000000000000 ) ) ;
#13787=CARTESIAN_POINT ( 'NONE',  ( 10.00000000000000000, -12.18267823974769293, 25.42247726998010648 ) ) ;
#13791=EDGE_CURVE ( 'NONE', #5783, #15756, #8387, .T. ) ;
#13798=CARTESIAN_POINT ( 'NONE',  ( 10.00000000000000000, 25.42247726998014912, 12.18267823974760411 ) ) ;
#13815=ORIENTED_EDGE ( 'NONE', *, *, #10399, .F. ) ;
#13826=FACE_OUTER_BOUND ( 'NONE', #15241, .T. ) ;
#13830=LINE ( 'NONE', #12409, #15071 ) ;
#13845=DIRECTION ( 'NONE',  ( -1.000000000000000000, 0.000000000000000000, 0.000000000000000000 ) ) ;
#13847=AXIS2_PLACEMENT_3D ( 'NONE', #13798, #18465, #5517 ) ;
#13871=EDGE_CURVE ( 'NONE', #6780, #17410, #5330, .T. ) ;
#13872=DIRECTION ( 'NONE',  ( -1.000000000000000000, -0.000000000000000000, 0.000000000000000000 ) ) ;
#13875=ORIENTED_EDGE ( 'NONE', *, *, #2708, .F. ) ;
#13883=AXIS2_PLACEMENT_3D ( 'NONE', #8937, #10188, #3055 ) ;
#13886=VERTEX_POINT ( 'NONE', #14133 ) ;
#13887=ADVANCED_FACE ( 'NONE', ( #15280 ), #1097, .T. ) ;
#13892=ORIENTED_EDGE ( 'NONE', *, *, #4202, .F. ) ;
#13897=EDGE_CURVE ( 'NONE', #5831, #13703, #17504, .T. ) ;
#13906=AXIS2_PLACEMENT_3D ( 'NONE', #10227, #11395, #8886 ) ;
#13918=ORIENTED_EDGE ( 'NONE', *, *, #15050, .F. ) ;
#13921=CARTESIAN_POINT ( 'NONE',  ( 0.000000000000000000, 5.086963483077590276, -27.72801475327276677 ) ) ;
#13922=CARTESIAN_POINT ( 'NONE',  ( 10.00000000000000000, -25.42247726998005675, -12.18267823974779240 ) ) ;
#13926=ORIENTED_EDGE ( 'NONE', *, *, #9491, .F. ) ;
#13933=AXIS2_PLACEMENT_3D ( 'NONE', #2105, #1719, #9329 ) ;
#13940=ORIENTED_EDGE ( 'NONE', *, *, #5768, .T. ) ;
#13949=CIRCLE ( 'NONE', #18194, 12.00000000001200462 ) ;
#13957=EDGE_CURVE ( 'NONE', #17358, #7974, #3762, .T. ) ;
#13959=AXIS2_PLACEMENT_3D ( 'NONE', #9222, #6559, #2270 ) ;
#13960=AXIS2_PLACEMENT_3D ( 'NONE', #4617, #10425, #5942 ) ;
#13961=AXIS2_PLACEMENT_3D ( 'NONE', #6189, #11907, #17807 ) ;
#13962=EDGE_LOOP ( 'NONE', ( #4835, #12585, #628, #1467 ) ) ;
#13969=ORIENTED_EDGE ( 'NONE', *, *, #17820, .F. ) ;
#13987=DIRECTION ( 'NONE',  ( 1.000000000000000000, -0.000000000000000000, -0.000000000000000000 ) ) ;
#13992=ORIENTED_EDGE ( 'NONE', *, *, #12161, .T. ) ;
#13995=EDGE_CURVE ( 'NONE', #10460, #6241, #2933, .T. ) ;
#14001=EDGE_LOOP ( 'NONE', ( #12030, #7670, #9550, #703 ) ) ;
#14010=DIRECTION ( 'NONE',  ( 0.000000000000000000, 0.000000000000000000, 1.000000000000000000 ) ) ;
#14012=EDGE_CURVE ( 'NONE', #10666, #4042, #1995, .T. ) ;
#14017=ADVANCED_FACE ( 'NONE', ( #10896 ), #2325, .T. ) ;
#14020=ORIENTED_EDGE ( 'NONE', *, *, #13532, .F. ) ;
#14021=EDGE_CURVE ( 'NONE', #8500, #9007, #17822, .T. ) ;
#14025=DIRECTION ( 'NONE',  ( 0.000000000000000000, 0.000000000000000000, 1.000000000000000000 ) ) ;
#14032=CARTESIAN_POINT ( 'NONE',  ( 0.000000000000000000, 29.03656532225563680, 15.68049343256006800 ) ) ;
#14035=ORIENTED_EDGE ( 'NONE', *, *, #1308, .F. ) ;
#14042=AXIS2_PLACEMENT_3D ( 'NONE', #10155, #14534, #1497 ) ;
#14043=CARTESIAN_POINT ( 'NONE',  ( 10.00000000000000000, 5.940243314904215310, 32.46095361140694990 ) ) ;
#14048=DIRECTION ( 'NONE',  ( 0.000000000000000000, 0.000000000000000000, 1.000000000000000000 ) ) ;
#14051=ORIENTED_EDGE ( 'NONE', *, *, #16713, .T. ) ;
#14062=VERTEX_POINT ( 'NONE', #7083 ) ;
#14072=LINE ( 'NONE', #9787, #2822 ) ;
#14073=CARTESIAN_POINT ( 'NONE',  ( 0.000000000000000000, 0.000000000000000000, 0.000000000000000000 ) ) ;
#14079=CARTESIAN_POINT ( 'NONE',  ( 10.00000000000000000, 29.75305054077471922, 14.27431201565535090 ) ) ;
#14082=DIRECTION ( 'NONE',  ( -1.000000000000000000, 0.000000000000000000, 0.000000000000000000 ) ) ;
#14088=ORIENTED_EDGE ( 'NONE', *, *, #16510, .T. ) ;
#14098=CARTESIAN_POINT ( 'NONE',  ( 10.00000000000000000, 6.681932690257323060, -25.38428207620315291 ) ) ;
#14105=ADVANCED_FACE ( 'NONE', ( #18614 ), #12999, .T. ) ;
#14112=CARTESIAN_POINT ( 'NONE',  ( 10.00000000000000000, 0.000000000000000000, 0.000000000000000000 ) ) ;
#14116=CARTESIAN_POINT ( 'NONE',  ( 0.000000000000000000, 0.000000000000000000, 0.000000000000000000 ) ) ;
#14118=ORIENTED_EDGE ( 'NONE', *, *, #3526, .T. ) ;
#14133=CARTESIAN_POINT ( 'NONE',  ( 0.000000000000000000, -29.03656532225574338, 15.68049343255986372 ) ) ;
#14136=DIRECTION ( 'NONE',  ( -1.000000000000000000, 0.000000000000000000, -0.000000000000000000 ) ) ;
#14153=ORIENTED_EDGE ( 'NONE', *, *, #6114, .T. ) ;
#14154=DIRECTION ( 'NONE',  ( -1.000000000000000000, -0.000000000000000000, 0.000000000000000000 ) ) ;
#14156=DIRECTION ( 'NONE',  ( 1.000000000000000000, 0.000000000000000000, -0.000000000000000000 ) ) ;
#14163=UNCERTAINTY_MEASURE_WITH_UNIT (LENGTH_MEASURE( 1.000000000000000082E-05 ), #3316, 'distance_accuracy_value', 'NONE');
#14169=EDGE_CURVE ( 'NONE', #5321, #6853, #17519, .T. ) ;
#14176=CYLINDRICAL_SURFACE ( 'NONE', #9319, 26.24900000002624978 ) ;
#14179=FACE_OUTER_BOUND ( 'NONE', #15495, .T. ) ;
#14181=AXIS2_PLACEMENT_3D ( 'NONE', #12116, #3457, #11746 ) ;
#14183=ADVANCED_FACE ( 'NONE', ( #13372 ), #1640, .F. ) ;
#14186=EDGE_LOOP ( 'NONE', ( #3629, #14051, #6528, #6491 ) ) ;
#14196=CARTESIAN_POINT ( 'NONE',  ( 5.000000000000000000, 22.76987570971527575, 23.88582760061489552 ) ) ;
#14203=FACE_OUTER_BOUND ( 'NONE', #7346, .T. ) ;
#14206=AXIS2_PLACEMENT_3D ( 'NONE', #12194, #772, #5142 ) ;
#14210=EDGE_CURVE ( 'NONE', #6839, #10560, #6569, .T. ) ;
#14212=CYLINDRICAL_SURFACE ( 'NONE', #13001, 26.24900000002624978 ) ;
#14215=EDGE_LOOP ( 'NONE', ( #6036, #11009, #11314, #3438 ) ) ;
#14218=AXIS2_PLACEMENT_3D ( 'NONE', #6172, #13708, #14944 ) ;
#14225=CARTESIAN_POINT ( 'NONE',  ( 5.000000000000000000, 32.70783759231086663, 4.381479206523104963 ) ) ;
#14226=EDGE_LOOP ( 'NONE', ( #9772, #12378, #11891, #10690 ) ) ;
#14236=AXIS2_PLACEMENT_3D ( 'NONE', #4078, #8545, #1586 ) ;
#14237=CIRCLE ( 'NONE', #14524, 33.00000000003299760 ) ;
#14242=DIRECTION ( 'NONE',  ( -1.000000000000000000, -0.000000000000000000, -0.000000000000000000 ) ) ;
#14243=DIRECTION ( 'NONE',  ( 0.000000000000000000, 0.9510565162951544194, -0.3090169943749447312 ) ) ;
#14245=CARTESIAN_POINT ( 'NONE',  ( 10.00000000000000000, 6.681932690256967788, 25.38428207620324883 ) ) ;
#14250=DIRECTION ( 'NONE',  ( 0.000000000000000000, -0.3090169943749546677, 0.9510565162951511997 ) ) ;
#14258=ADVANCED_FACE ( 'NONE', ( #4686 ), #16135, .T. ) ;
#14260=FACE_OUTER_BOUND ( 'NONE', #14215, .T. ) ;
#14261=ADVANCED_FACE ( 'NONE', ( #9072 ), #8879, .T. ) ;
#14263=EDGE_CURVE ( 'NONE', #12365, #4436, #9631, .T. ) ;
#14266=AXIS2_PLACEMENT_3D ( 'NONE', #2363, #5308, #3991 ) ;
#14282=VERTEX_POINT ( 'NONE', #10681 ) ;
#14289=EDGE_CURVE ( 'NONE', #18064, #15756, #10963, .T. ) ;
#14291=VERTEX_POINT ( 'NONE', #15549 ) ;
#14300=DIRECTION ( 'NONE',  ( 0.000000000000000000, 0.9510565162951543083, -0.3090169943749447867 ) ) ;
#14302=LINE ( 'NONE', #14098, #4544 ) ;
#14305=AXIS2_PLACEMENT_3D ( 'NONE', #8527, #8619, #13236 ) ;
#14322=EDGE_LOOP ( 'NONE', ( #11924, #2168, #8278, #1135 ) ) ;
#14324=DIRECTION ( 'NONE',  ( 0.000000000000000000, 0.000000000000000000, 1.000000000000000000 ) ) ;
#14332=DIRECTION ( 'NONE',  ( 1.000000000000000000, 0.000000000000000000, 0.000000000000000000 ) ) ;
#14336=CIRCLE ( 'NONE', #16774, 12.00000000001200462 ) ;
#14343=EDGE_LOOP ( 'NONE', ( #777, #10867, #16782, #2664 ) ) ;
#14347=EDGE_CURVE ( 'NONE', #10957, #13630, #9535, .T. ) ;
#14349=ADVANCED_FACE ( 'NONE', ( #8116 ), #5060, .T. ) ;
#14355=CARTESIAN_POINT ( 'NONE',  ( 0.000000000000000000, -24.79895094899269026, 13.40641754777657013 ) ) ;
#14356=ORIENTED_EDGE ( 'NONE', *, *, #3767, .F. ) ;
#14364=DIRECTION ( 'NONE',  ( -1.000000000000000000, -0.000000000000000000, -0.000000000000000000 ) ) ;
#14369=AXIS2_PLACEMENT_3D ( 'NONE', #2673, #16966, #6855 ) ;
#14370=EDGE_CURVE ( 'NONE', #11328, #16693, #14501, .T. ) ;
#14375=ORIENTED_EDGE ( 'NONE', *, *, #8068, .F. ) ;
#14381=DIRECTION ( 'NONE',  ( 0.000000000000000000, -0.5877852522924802425, 0.8090169943749422332 ) ) ;
#14383=CIRCLE ( 'NONE', #6470, 12.00000000001200817 ) ;
#14386=AXIS2_PLACEMENT_3D ( 'NONE', #13922, #1063, #3821 ) ;
#14392=CARTESIAN_POINT ( 'NONE',  ( 50.00005079999999680, 0.000000000000000000, 0.000000000000000000 ) ) ;
#14404=DIRECTION ( 'NONE',  ( 1.000000000000000000, 0.000000000000000000, 0.000000000000000000 ) ) ;
#14408=EDGE_CURVE ( 'NONE', #13712, #10104, #8716, .T. ) ;
#14409=AXIS2_PLACEMENT_3D ( 'NONE', #332, #419, #15192 ) ;
#14413=ORIENTED_EDGE ( 'NONE', *, *, #2712, .F. ) ;
#14424=CYLINDRICAL_SURFACE ( 'NONE', #8324, 33.00000000003299760 ) ;
#14433=CARTESIAN_POINT ( 'NONE',  ( 0.000000000000000000, -26.20671763660629594, 1.489278925039428936 ) ) ;
#14435=ORIENTED_EDGE ( 'NONE', *, *, #3101, .T. ) ;
#14449=PRODUCT_DEFINITION_FORMATION_WITH_SPECIFIED_SOURCE ( 'ANY', '', #15750, .NOT_KNOWN. ) ;
#14460=DIRECTION ( 'NONE',  ( -1.000000000000000000, 0.000000000000000000, -0.000000000000000000 ) ) ;
#14465=DIRECTION ( 'NONE',  ( 0.000000000000000000, -0.3090169943749349613, -0.9510565162951576390 ) ) ;
#14471=EDGE_LOOP ( 'NONE', ( #1669, #10540, #181, #1993 ) ) ;
#14486=DIRECTION ( 'NONE',  ( -1.000000000000000000, 0.000000000000000000, 0.000000000000000000 ) ) ;
#14501=CIRCLE ( 'NONE', #15714, 12.00000000001200640 ) ;
#14505=ORIENTED_EDGE ( 'NONE', *, *, #6072, .F. ) ;
#14506=AXIS2_PLACEMENT_3D ( 'NONE', #14112, #9743, #15902 ) ;
#14507=ADVANCED_FACE ( 'NONE', ( #17360 ), #8498, .T. ) ;
#14513=CARTESIAN_POINT ( 'NONE',  ( 10.00000000000000000, 26.20671763660628528, -1.489278925039611901 ) ) ;
#14524=AXIS2_PLACEMENT_3D ( 'NONE', #11463, #10126, #2701 ) ;
#14534=DIRECTION ( 'NONE',  ( -1.000000000000000000, 0.000000000000000000, 0.000000000000000000 ) ) ;
#14547=EDGE_CURVE ( 'NONE', #3169, #16256, #16619, .T. ) ;
#14548=CARTESIAN_POINT ( 'NONE',  ( 10.00000000000000000, 1.489278925039883239, -26.20671763660627107 ) ) ;
#14551=VECTOR ( 'NONE', #8614, 1000.000000000000000 ) ;
#14565=AXIS2_PLACEMENT_3D ( 'NONE', #16260, #172, #13132 ) ;
#14573=CARTESIAN_POINT ( 'NONE',  ( 10.00000000000000000, -29.03656532225551601, -15.68049343256028294 ) ) ;
#14579=AXIS2_PLACEMENT_3D ( 'NONE', #10397, #6295, #9057 ) ;
#14584=ORIENTED_EDGE ( 'NONE', *, *, #11210, .T. ) ;
#14585=( NAMED_UNIT ( * ) SI_UNIT ( $, .STERADIAN. ) SOLID_ANGLE_UNIT ( ) );
#14586=EDGE_CURVE ( 'NONE', #6251, #5299, #5460, .T. ) ;
#14590=LINE ( 'NONE', #11554, #15762 ) ;
#14593=DIRECTION ( 'NONE',  ( -1.000000000000000000, -0.000000000000000000, 0.000000000000000000 ) ) ;
#14595=DIRECTION ( 'NONE',  ( 1.000000000000000000, -0.000000000000000000, -0.000000000000000000 ) ) ;
#14597=ADVANCED_FACE ( 'NONE', ( #11444 ), #14212, .T. ) ;
#14598=DIRECTION ( 'NONE',  ( -1.000000000000000000, -0.000000000000000000, 0.000000000000000000 ) ) ;
#14601=SHAPE_DEFINITION_REPRESENTATION ( #12862, #13460 ) ;
#14609=FACE_OUTER_BOUND ( 'NONE', #2292, .T. ) ;
#14637=LINE ( 'NONE', #7395, #15395 ) ;
#14641=EDGE_CURVE ( 'NONE', #12365, #18659, #12255, .T. ) ;
#14644=ORIENTED_EDGE ( 'NONE', *, *, #6030, .T. ) ;
#14647=AXIS2_PLACEMENT_3D ( 'NONE', #16721, #12228, #9656 ) ;
#14653=DIRECTION ( 'NONE',  ( 0.000000000000000000, 0.3090169943749411785, 0.9510565162951556406 ) ) ;
#14656=ORIENTED_EDGE ( 'NONE', *, *, #4202, .T. ) ;
#14667=DIRECTION ( 'NONE',  ( 0.000000000000000000, 0.000000000000000000, 1.000000000000000000 ) ) ;
#14668=CARTESIAN_POINT ( 'NONE',  ( 10.00000000000000000, 24.79895094899259789, -13.40641754777674421 ) ) ;
#14676=CYLINDRICAL_SURFACE ( 'NONE', #16925, 33.00000000003299760 ) ;
#14679=LINE ( 'NONE', #13253, #3521 ) ;
#14706=LINE ( 'NONE', #519, #9972 ) ;
#14707=ORIENTED_EDGE ( 'NONE', *, *, #8679, .T. ) ;
#14708=ORIENTED_EDGE ( 'NONE', *, *, #16702, .F. ) ;
#14715=EDGE_CURVE ( 'NONE', #11197, #12068, #5699, .T. ) ;
#14719=CARTESIAN_POINT ( 'NONE',  ( 5.000000000000000000, -4.381479206522763015, -32.70783759231090926 ) ) ;
#14722=DIRECTION ( 'NONE',  ( 0.000000000000000000, 0.000000000000000000, 1.000000000000000000 ) ) ;
#14723=ORIENTED_EDGE ( 'NONE', *, *, #5887, .T. ) ;
#14725=ORIENTED_EDGE ( 'NONE', *, *, #8492, .F. ) ;
#14735=DIRECTION ( 'NONE',  ( -1.000000000000000000, -0.000000000000000000, -0.000000000000000000 ) ) ;
#14738=ORIENTED_EDGE ( 'NONE', *, *, #4470, .T. ) ;
#14745=DIRECTION ( 'NONE',  ( 0.000000000000000000, -0.8090169943749402348, -0.5877852522924831291 ) ) ;
#14749=DIRECTION ( 'NONE',  ( -1.000000000000000000, 0.000000000000000000, 0.000000000000000000 ) ) ;
#14761=DIRECTION ( 'NONE',  ( -1.000000000000000000, -0.000000000000000000, -0.000000000000000000 ) ) ;
#14765=AXIS2_PLACEMENT_3D ( 'NONE', #9524, #12102, #17918 ) ;
#14767=CARTESIAN_POINT ( 'NONE',  ( 10.00000000000000178, 0.000000000000000000, 5.000000000000000000 ) ) ;
#14781=EDGE_LOOP ( 'NONE', ( #1952, #13875, #17951, #16422 ) ) ;
#14782=VERTEX_POINT ( 'NONE', #17036 ) ;
#14810=CIRCLE ( 'NONE', #7454, 33.00000000003299760 ) ;
#14824=EDGE_CURVE ( 'NONE', #808, #15251, #15429, .T. ) ;
#14828=CIRCLE ( 'NONE', #7830, 12.00000000001200640 ) ;
#14830=ORIENTED_EDGE ( 'NONE', *, *, #9563, .F. ) ;
#14837=AXIS2_PLACEMENT_3D ( 'NONE', #751, #7977, #3790 ) ;
#14844=ORIENTED_EDGE ( 'NONE', *, *, #6568, .T. ) ;
#14847=DIRECTION ( 'NONE',  ( 0.000000000000000000, 0.000000000000000000, -1.000000000000000000 ) ) ;
#14851=DIRECTION ( 'NONE',  ( 0.000000000000000000, 0.9510565162951523099, 0.3090169943749515591 ) ) ;
#14857=CARTESIAN_POINT ( 'NONE',  ( 10.00000000000000000, 5.086963483077590276, -27.72801475327276677 ) ) ;
#14862=MECHANICAL_DESIGN_GEOMETRIC_PRESENTATION_REPRESENTATION('',(#10302),#3605);
#14880=LINE ( 'NONE', #1914, #1199 ) ;
#14891=DIRECTION ( 'NONE',  ( -1.000000000000000000, -0.000000000000000000, 0.000000000000000000 ) ) ;
#14900=DIRECTION ( 'NONE',  ( 0.000000000000000000, 1.000000000000000000, 3.491481338843133355E-15 ) ) ;
#14912=VERTEX_POINT ( 'NONE', #12636 ) ;
#14914=AXIS2_PLACEMENT_3D ( 'NONE', #2519, #9948, #14048 ) ;
#14918=EDGE_LOOP ( 'NONE', ( #8236, #8366, #14644, #10807 ) ) ;
#14929=PRESENTATION_STYLE_ASSIGNMENT (( #15217 ) ) ;
#14930=ORIENTED_EDGE ( 'NONE', *, *, #1801, .F. ) ;
#14944=DIRECTION ( 'NONE',  ( 0.000000000000000000, 0.000000000000000000, 1.000000000000000000 ) ) ;
#14949=CARTESIAN_POINT ( 'NONE',  ( 10.00000000000000000, -27.94286728106390072, -3.730438010304629515 ) ) ;
#14956=AXIS2_PLACEMENT_3D ( 'NONE', #32, #10205, #1183 ) ;
#14958=EDGE_CURVE ( 'NONE', #8129, #10560, #10247, .T. ) ;
#14960=ORIENTED_EDGE ( 'NONE', *, *, #7423, .F. ) ;
#14967=CYLINDRICAL_SURFACE ( 'NONE', #17310, 33.00000000003299760 ) ;
#14968=FACE_OUTER_BOUND ( 'NONE', #11435, .T. ) ;
#14972=ORIENTED_EDGE ( 'NONE', *, *, #2262, .F. ) ;
#14980=VERTEX_POINT ( 'NONE', #4351 ) ;
#14982=CYLINDRICAL_SURFACE ( 'NONE', #6715, 12.00000000001200462 ) ;
#14984=EDGE_CURVE ( 'NONE', #10779, #15019, #10151, .T. ) ;
#14987=DIRECTION ( 'NONE',  ( -1.000000000000000000, 0.000000000000000000, 0.000000000000000000 ) ) ;
#14996=DIRECTION ( 'NONE',  ( -1.000000000000000000, -0.000000000000000000, -0.000000000000000000 ) ) ;
#14997=VERTEX_POINT ( 'NONE', #13297 ) ;
#15013=FACE_OUTER_BOUND ( 'NONE', #12597, .T. ) ;
#15019=VERTEX_POINT ( 'NONE', #4536 ) ;
#15026=DIRECTION ( 'NONE',  ( -1.000000000000000000, -0.000000000000000000, 0.000000000000000000 ) ) ;
#15031=CARTESIAN_POINT ( 'NONE',  ( 0.000000000000000000, 0.000000000000000000, 0.000000000000000000 ) ) ;
#15034=CARTESIAN_POINT ( 'NONE',  ( 0.000000000000000000, 0.000000000000000000, 0.000000000000000000 ) ) ;
#15035=CARTESIAN_POINT ( 'NONE',  ( 0.000000000000000000, 4.381479206522993941, 32.70783759231088084 ) ) ;
#15037=FACE_OUTER_BOUND ( 'NONE', #15602, .T. ) ;
#15039=EDGE_CURVE ( 'NONE', #4267, #726, #4786, .T. ) ;
#15041=EDGE_CURVE ( 'NONE', #8001, #5512, #5997, .T. ) ;
#15050=EDGE_CURVE ( 'NONE', #8889, #5171, #14828, .T. ) ;
#15057=CIRCLE ( 'NONE', #12625, 12.00000000001200462 ) ;
#15063=CARTESIAN_POINT ( 'NONE',  ( 0.000000000000000000, -6.681932690256794594, -25.38428207620328791 ) ) ;
#15065=EDGE_CURVE ( 'NONE', #13152, #14782, #7150, .T. ) ;
#15071=VECTOR ( 'NONE', #5557, 1000.000000000000000 ) ;
#15101=AXIS2_PLACEMENT_3D ( 'NONE', #14857, #7696, #13519 ) ;
#15112=FACE_BOUND ( 'NONE', #5366, .T. ) ;
#15113=ORIENTED_EDGE ( 'NONE', *, *, #13439, .T. ) ;
#15117=ORIENTED_EDGE ( 'NONE', *, *, #1391, .T. ) ;
#15123=AXIS2_PLACEMENT_3D ( 'NONE', #3634, #9428, #15246 ) ;
#15133=CARTESIAN_POINT ( 'NONE',  ( 10.00000000000000000, -19.44239304137390434, 20.41355805489607889 ) ) ;
#15142=DIRECTION ( 'NONE',  ( 0.000000000000000000, 0.000000000000000000, 1.000000000000000000 ) ) ;
#15143=EDGE_CURVE ( 'NONE', #17590, #16428, #16245, .T. ) ;
#15148=CIRCLE ( 'NONE', #16365, 33.00000000003299760 ) ;
#15152=VECTOR ( 'NONE', #4252, 1000.000000000000000 ) ;
#15159=CIRCLE ( 'NONE', #11207, 33.00000000003299760 ) ;
#15171=EDGE_LOOP ( 'NONE', ( #17244, #18058, #2133, #13203 ) ) ;
#15172=AXIS2_PLACEMENT_3D ( 'NONE', #6269, #659, #11806 ) ;
#15186=LINE ( 'NONE', #16506, #12319 ) ;
#15192=DIRECTION ( 'NONE',  ( 0.000000000000000000, 0.000000000000000000, 1.000000000000000000 ) ) ;
#15198=CARTESIAN_POINT ( 'NONE',  ( 50.00005079999999680, 6.799999999999999822, 1.500000000000000000 ) ) ;
#15202=DIRECTION ( 'NONE',  ( 0.000000000000000000, 0.000000000000000000, -1.000000000000000000 ) ) ;
#15206=CARTESIAN_POINT ( 'NONE',  ( 10.00000000000000000, -9.514709542737069370, 24.46385708179980512 ) ) ;
#15207=VERTEX_POINT ( 'NONE', #7578 ) ;
#15217=SURFACE_STYLE_USAGE ( .BOTH. , #13694 ) ;
#15218=EDGE_LOOP ( 'NONE', ( #10029, #13264, #2248, #18694 ) ) ;
#15219=CARTESIAN_POINT ( 'NONE',  ( 10.00000000000000000, -15.68049343255974826, -29.03656532225580733 ) ) ;
#15226=CARTESIAN_POINT ( 'NONE',  ( 10.00000000000000000, -5.086963483077008519, -27.72801475327286980 ) ) ;
#15230=EDGE_CURVE ( 'NONE', #3488, #17821, #16438, .T. ) ;
#15233=CYLINDRICAL_SURFACE ( 'NONE', #2017, 12.00000000001200107 ) ;
#15234=ORIENTED_EDGE ( 'NONE', *, *, #17820, .T. ) ;
#15235=DIRECTION ( 'NONE',  ( -1.000000000000000000, 0.000000000000000000, 0.000000000000000000 ) ) ;
#15241=EDGE_LOOP ( 'NONE', ( #3702, #7115, #16918, #1748 ) ) ;
#15246=DIRECTION ( 'NONE',  ( 0.000000000000000000, 0.000000000000000000, 1.000000000000000000 ) ) ;
#15251=VERTEX_POINT ( 'NONE', #11185 ) ;
#15252=DIRECTION ( 'NONE',  ( 0.000000000000000000, 0.3090169943749479509, -0.9510565162951533091 ) ) ;
#15257=EDGE_LOOP ( 'NONE', ( #4287, #11964, #5489, #10288 ) ) ;
#15259=CARTESIAN_POINT ( 'NONE',  ( 10.00000000000000000, 0.000000000000000000, 0.000000000000000000 ) ) ;
#15269=VERTEX_POINT ( 'NONE', #17015 ) ;
#15270=ORIENTED_EDGE ( 'NONE', *, *, #14263, .F. ) ;
#15280=FACE_OUTER_BOUND ( 'NONE', #5396, .T. ) ;
#15288=CIRCLE ( 'NONE', #1903, 12.00000000001200284 ) ;
#15295=DIRECTION ( 'NONE',  ( 1.000000000000000000, 0.000000000000000000, 0.000000000000000000 ) ) ;
#15303=AXIS2_PLACEMENT_3D ( 'NONE', #4721, #6353, #10533 ) ;
#15310=ORIENTED_EDGE ( 'NONE', *, *, #15871, .T. ) ;
#15315=CYLINDRICAL_SURFACE ( 'NONE', #6074, 12.00000000001200284 ) ;
#15320=VERTEX_POINT ( 'NONE', #16727 ) ;
#15326=EDGE_CURVE ( 'NONE', #15019, #12930, #6333, .T. ) ;
#15331=FACE_OUTER_BOUND ( 'NONE', #334, .T. ) ;
#15337=CARTESIAN_POINT ( 'NONE',  ( 10.00000000000000000, -22.07705612348849655, 14.19907017806860949 ) ) ;
#15341=ORIENTED_EDGE ( 'NONE', *, *, #4124, .T. ) ;
#15344=DIRECTION ( 'NONE',  ( 0.000000000000000000, 0.000000000000000000, 1.000000000000000000 ) ) ;
#15356=EDGE_CURVE ( 'NONE', #5321, #6583, #2231, .T. ) ;
#15357=EDGE_CURVE ( 'NONE', #13630, #16495, #3291, .T. ) ;
#15360=ORIENTED_EDGE ( 'NONE', *, *, #1967, .T. ) ;
#15368=CIRCLE ( 'NONE', #11413, 33.00000000003299760 ) ;
#15372=CIRCLE ( 'NONE', #11118, 12.00000000001200640 ) ;
#15375=DIRECTION ( 'NONE',  ( 0.000000000000000000, -0.9510565162951502005, -0.3090169943749581649 ) ) ;
#15380=AXIS2_PLACEMENT_3D ( 'NONE', #11831, #17640, #12386 ) ;
#15388=CARTESIAN_POINT ( 'NONE',  ( 0.000000000000000000, 5.086963483077203918, 27.72801475327284138 ) ) ;
#15389=ORIENTED_EDGE ( 'NONE', *, *, #7615, .F. ) ;
#15390=CARTESIAN_POINT ( 'NONE',  ( 5.000000000000000000, 23.88582760061514421, -22.76987570971501640 ) ) ;
#15395=VECTOR ( 'NONE', #13211, 1000.000000000000000 ) ;
#15396=AXIS2_PLACEMENT_3D ( 'NONE', #16185, #13428, #8846 ) ;
#15410=CIRCLE ( 'NONE', #10242, 12.00000000001200462 ) ;
#15412=LINE ( 'NONE', #8178, #10548 ) ;
#15415=EDGE_CURVE ( 'NONE', #16428, #10912, #12726, .T. ) ;
#15416=FACE_OUTER_BOUND ( 'NONE', #12823, .T. ) ;
#15418=VECTOR ( 'NONE', #11155, 1000.000000000000000 ) ;
#15421=AXIS2_PLACEMENT_3D ( 'NONE', #7908, #16861, #6480 ) ;
#15428=CIRCLE ( 'NONE', #1439, 5.000000000000000000 ) ;
#15429=CIRCLE ( 'NONE', #18775, 12.00000000001200817 ) ;
#15440=ORIENTED_EDGE ( 'NONE', *, *, #3280, .T. ) ;
#15450=ORIENTED_EDGE ( 'NONE', *, *, #868, .F. ) ;
#15473=CARTESIAN_POINT ( 'NONE',  ( 10.00000000000000000, -13.40641754777648487, -24.79895094899273644 ) ) ;
#15478=EDGE_CURVE ( 'NONE', #1304, #726, #17291, .T. ) ;
#15489=DIRECTION ( 'NONE',  ( -1.000000000000000000, -0.000000000000000000, -0.000000000000000000 ) ) ;
#15495=EDGE_LOOP ( 'NONE', ( #18344, #18016, #7398, #17256 ) ) ;
#15500=DIRECTION ( 'NONE',  ( 0.000000000000000000, 0.9510565162951543083, -0.3090169943749447312 ) ) ;
#15507=CARTESIAN_POINT ( 'NONE',  ( 10.00000000000000000, 0.000000000000000000, 0.000000000000000000 ) ) ;
#15508=ORIENTED_EDGE ( 'NONE', *, *, #16460, .F. ) ;
#15517=DIRECTION ( 'NONE',  ( -1.000000000000000000, 0.000000000000000000, 0.000000000000000000 ) ) ;
#15518=DIRECTION ( 'NONE',  ( 0.000000000000000000, 0.8090169943749486725, -0.5877852522924712497 ) ) ;
#15522=AXIS2_PLACEMENT_3D ( 'NONE', #18713, #4524, #144 ) ;
#15524=EDGE_CURVE ( 'NONE', #1965, #18064, #11797, .T. ) ;
#15526=ADVANCED_FACE ( 'NONE', ( #14609 ), #1290, .T. ) ;
#15527=ORIENTED_EDGE ( 'NONE', *, *, #10293, .F. ) ;
#15532=EDGE_CURVE ( 'NONE', #262, #5512, #1375, .T. ) ;
#15538=DIRECTION ( 'NONE',  ( 0.000000000000000000, 0.5877852522924742473, -0.8090169943749465631 ) ) ;
#15539=DIRECTION ( 'NONE',  ( -1.000000000000000000, 0.000000000000000000, 0.000000000000000000 ) ) ;
#15549=CARTESIAN_POINT ( 'NONE',  ( 0.000000000000000000, -32.70783759231083820, -4.381479206523335890 ) ) ;
#15552=CARTESIAN_POINT ( 'NONE',  ( 10.00000000000000000, 9.514709542736897063, 24.46385708179987262 ) ) ;
#15558=CARTESIAN_POINT ( 'NONE',  ( 0.000000000000000000, 0.000000000000000000, 0.000000000000000000 ) ) ;
#15559=VERTEX_POINT ( 'NONE', #12118 ) ;
#15566=CARTESIAN_POINT ( 'NONE',  ( 10.00000000000000000, -22.76987570971509456, -23.88582760061506249 ) ) ;
#15570=DIRECTION ( 'NONE',  ( 0.000000000000000000, 0.8090169943749486725, -0.5877852522924712497 ) ) ;
#15574=CIRCLE ( 'NONE', #14647, 12.00000000001200640 ) ;
#15578=CARTESIAN_POINT ( 'NONE',  ( 0.000000000000000000, -22.07705612348829050, -14.19907017806892924 ) ) ;
#15580=DIRECTION ( 'NONE',  ( -1.000000000000000000, 0.000000000000000000, 0.000000000000000000 ) ) ;
#15598=DIRECTION ( 'NONE',  ( 0.000000000000000000, 0.3090169943749481174, -0.9510565162951533091 ) ) ;
#15599=DIRECTION ( 'NONE',  ( -1.000000000000000000, 0.000000000000000000, 0.000000000000000000 ) ) ;
#15602=EDGE_LOOP ( 'NONE', ( #8456, #5383, #10385, #1058 ) ) ;
#15603=CARTESIAN_POINT ( 'NONE',  ( 0.000000000000000000, -27.72801475327285559, 5.086963483077107995 ) ) ;
#15604=DIRECTION ( 'NONE',  ( 0.000000000000000000, 0.000000000000000000, -1.000000000000000000 ) ) ;
#15606=ORIENTED_EDGE ( 'NONE', *, *, #3101, .F. ) ;
#15614=CLOSED_SHELL ( 'NONE', ( #6364, #1535, #3673, #12374, #8718, #140, #3549, #18787, #5838, #14183, #9043, #2970, #10882, #17122, #7368, #7695, #8942, #16718, #11632, #7376, #17299, #15526, #2965, #6279, #11212, #3909, #5273, #2069, #18323, #2027, #5860, #4976, #6716, #10321, #2250, #9605, #16198, #3778, #18494, #11700, #13887, #1563, #8756, #8523, #15980, #14349, #17861, #5384, #9529, #3522, #6192, #7029, #9532, #8218, #18613, #9697, #14258, #12141, #3552, #9850, #46, #3317, #14261, #2368, #10016, #14017, #6930, #1357, #228, #3760, #2689, #18547, #10020, #1080, #8785, #16283, #8003, #1434, #11975, #6336, #14597, #5473, #11758, #10855, #7312, #14507, #12514, #3622, #13144, #3781, #5220, #14105, #7968 ) ) ;
#15625=DIRECTION ( 'NONE',  ( 1.000000000000000000, -0.000000000000000000, -0.000000000000000000 ) ) ;
#15626=DIRECTION ( 'NONE',  ( -1.000000000000000000, 0.000000000000000000, -0.000000000000000000 ) ) ;
#15651=CARTESIAN_POINT ( 'NONE',  ( 0.000000000000000000, -27.94286728106395756, 15.73043801031622912 ) ) ;
#15663=DIRECTION ( 'NONE',  ( 0.000000000000000000, 0.000000000000000000, 1.000000000000000000 ) ) ;
#15666=LINE ( 'NONE', #14245, #14551 ) ;
#15678=EDGE_LOOP ( 'NONE', ( #4176, #9171, #10207, #7637 ) ) ;
#15692=CARTESIAN_POINT ( 'NONE',  ( 10.00000000000000000, 25.42247726998014912, 12.18267823974760411 ) ) ;
#15696=CIRCLE ( 'NONE', #3523, 12.00000000001200462 ) ;
#15700=EDGE_CURVE ( 'NONE', #9007, #15320, #15159, .T. ) ;
#15706=VECTOR ( 'NONE', #15202, 1000.000000000000000 ) ;
#15708=APPLICATION_CONTEXT ( 'automotive_design' ) ;
#15709=CIRCLE ( 'NONE', #11127, 12.00000000001200462 ) ;
#15713=VECTOR ( 'NONE', #18596, 1000.000000000000000 ) ;
#15714=AXIS2_PLACEMENT_3D ( 'NONE', #18388, #6494, #5347 ) ;
#15717=AXIS2_PLACEMENT_3D ( 'NONE', #18338, #7285, #1481 ) ;
#15719=DIRECTION ( 'NONE',  ( 0.000000000000000000, -0.9510565162951500895, -0.3090169943749581649 ) ) ;
#15735=ORIENTED_EDGE ( 'NONE', *, *, #12370, .T. ) ;
#15737=CYLINDRICAL_SURFACE ( 'NONE', #9141, 26.24900000002624978 ) ;
#15746=CARTESIAN_POINT ( 'NONE',  ( 10.00000000000000000, -27.72801475327278453, -5.086963483077506787 ) ) ;
#15747=ORIENTED_EDGE ( 'NONE', *, *, #3498, .F. ) ;
#15750=PRODUCT ( 'spur gear_iso_ISO - Spur gear 3M 20T 20PA 10FW ---S20A75H50L10.0S1', 'spur gear_iso_ISO - Spur gear 3M 20T 20PA 10FW ---S20A75H50L10.0S1', '', ( #1283 ) ) ;
#15756=VERTEX_POINT ( 'NONE', #16881 ) ;
#15762=VECTOR ( 'NONE', #31, 1000.000000000000000 ) ;
#15770=DIRECTION ( 'NONE',  ( 1.000000000000000000, -0.000000000000000000, 0.000000000000000000 ) ) ;
#15772=AXIS2_PLACEMENT_3D ( 'NONE', #10480, #16299, #7719 ) ;
#15776=CARTESIAN_POINT ( 'NONE',  ( 10.00000000000000000, -27.72801475327285559, 5.086963483077107995 ) ) ;
#15795=EDGE_LOOP ( 'NONE', ( #9024, #17500, #7267, #17817 ) ) ;
#15805=ORIENTED_EDGE ( 'NONE', *, *, #5887, .F. ) ;
#15810=EDGE_CURVE ( 'NONE', #7876, #15559, #3301, .T. ) ;
#15847=MANIFOLD_SOLID_BREP ( 'Keyway', #15614 ) ;
#15862=EDGE_CURVE ( 'NONE', #14912, #9858, #1271, .T. ) ;
#15870=VERTEX_POINT ( 'NONE', #1450 ) ;
#15871=EDGE_CURVE ( 'NONE', #15970, #11257, #9375, .T. ) ;
#15877=VECTOR ( 'NONE', #18658, 1000.000000000000000 ) ;
#15888=ORIENTED_EDGE ( 'NONE', *, *, #6450, .F. ) ;
#15889=DIRECTION ( 'NONE',  ( -1.000000000000000000, 0.000000000000000000, -0.000000000000000000 ) ) ;
#15899=ORIENTED_EDGE ( 'NONE', *, *, #7405, .F. ) ;
#15900=FACE_OUTER_BOUND ( 'NONE', #6151, .T. ) ;
#15902=DIRECTION ( 'NONE',  ( 0.000000000000000000, 0.5877852522924684742, 0.8090169943749506709 ) ) ;
#15904=CARTESIAN_POINT ( 'NONE',  ( 10.00000000000000000, -25.42247726998005675, -12.18267823974779240 ) ) ;
#15908=CARTESIAN_POINT ( 'NONE',  ( 10.00000000000000000, -14.19907017806852245, -22.07705612348854984 ) ) ;
#15909=ORIENTED_EDGE ( 'NONE', *, *, #1098, .F. ) ;
#15911=DIRECTION ( 'NONE',  ( 0.000000000000000000, 0.000000000000000000, 1.000000000000000000 ) ) ;
#15937=ORIENTED_EDGE ( 'NONE', *, *, #6267, .T. ) ;
#15941=CYLINDRICAL_SURFACE ( 'NONE', #6999, 12.00000000001200462 ) ;
#15944=DIRECTION ( 'NONE',  ( -1.000000000000000000, -0.000000000000000000, 0.000000000000000000 ) ) ;
#15950=DIRECTION ( 'NONE',  ( 0.000000000000000000, 0.000000000000000000, 1.000000000000000000 ) ) ;
#15970=VERTEX_POINT ( 'NONE', #4671 ) ;
#15977=AXIS2_PLACEMENT_3D ( 'NONE', #8351, #6536, #8060 ) ;
#15980=ADVANCED_FACE ( 'NONE', ( #9234 ), #6102, .T. ) ;
#15987=CYLINDRICAL_SURFACE ( 'NONE', #5373, 12.00000000001200462 ) ;
#15991=DIRECTION ( 'NONE',  ( 0.000000000000000000, 0.000000000000000000, 1.000000000000000000 ) ) ;
#15993=CARTESIAN_POINT ( 'NONE',  ( 0.000000000000000000, 27.72801475327274900, 5.086963483077687975 ) ) ;
#15996=AXIS2_PLACEMENT_3D ( 'NONE', #7276, #11655, #2713 ) ;
#15999=CARTESIAN_POINT ( 'NONE',  ( 10.00000000000000000, 25.38428207620331634, -6.681932690256706664 ) ) ;
#16007=EDGE_CURVE ( 'NONE', #4065, #12365, #3323, .T. ) ;
#16008=AXIS2_PLACEMENT_3D ( 'NONE', #6408, #12406, #12212 ) ;
#16023=AXIS2_PLACEMENT_3D ( 'NONE', #17620, #4567, #7054 ) ;
#16030=CIRCLE ( 'NONE', #15421, 12.00000000001200462 ) ;
#16033=AXIS2_PLACEMENT_3D ( 'NONE', #5013, #12263, #10822 ) ;
#16037=DIRECTION ( 'NONE',  ( 0.000000000000000000, 0.000000000000000000, -1.000000000000000000 ) ) ;
#16048=CARTESIAN_POINT ( 'NONE',  ( 10.00000000000000000, 20.41355805489615705, 19.44239304137382973 ) ) ;
#16055=ORIENTED_EDGE ( 'NONE', *, *, #17493, .T. ) ;
#16061=DIRECTION ( 'NONE',  ( 0.000000000000000000, -0.8090169943749401238, -0.5877852522924831291 ) ) ;
#16065=CARTESIAN_POINT ( 'NONE',  ( 0.000000000000000000, 0.000000000000000000, 0.000000000000000000 ) ) ;
#16069=CIRCLE ( 'NONE', #7855, 26.24900000002624978 ) ;
#16073=DIRECTION ( 'NONE',  ( 0.000000000000000000, -0.3090169943749546677, 0.9510565162951511997 ) ) ;
#16079=LINE ( 'NONE', #3215, #6360 ) ;
#16080=VECTOR ( 'NONE', #11062, 1000.000000000000000 ) ;
#16088=DIRECTION ( 'NONE',  ( -1.000000000000000000, -0.000000000000000000, 0.000000000000000000 ) ) ;
#16089=DIRECTION ( 'NONE',  ( 0.000000000000000000, 0.000000000000000000, -1.000000000000000000 ) ) ;
#16104=DIRECTION ( 'NONE',  ( 0.000000000000000000, 0.000000000000000000, 1.000000000000000000 ) ) ;
#16106=AXIS2_PLACEMENT_3D ( 'NONE', #10760, #18100, #15252 ) ;
#16118=DIRECTION ( 'NONE',  ( 0.000000000000000000, 0.000000000000000000, 1.000000000000000000 ) ) ;
#16119=ORIENTED_EDGE ( 'NONE', *, *, #11285, .F. ) ;
#16135=CYLINDRICAL_SURFACE ( 'NONE', #510, 26.24900000002624978 ) ;
#16168=EDGE_CURVE ( 'NONE', #14997, #4430, #12770, .T. ) ;
#16169=VERTEX_POINT ( 'NONE', #8380 ) ;
#16173=FACE_OUTER_BOUND ( 'NONE', #1824, .T. ) ;
#16185=CARTESIAN_POINT ( 'NONE',  ( 0.000000000000000000, 27.94286728106393269, 3.730438010304423013 ) ) ;
#16198=ADVANCED_FACE ( 'NONE', ( #11530 ), #4290, .T. ) ;
#16214=VECTOR ( 'NONE', #18248, 1000.000000000000000 ) ;
#16217=ORIENTED_EDGE ( 'NONE', *, *, #8931, .F. ) ;
#16220=DIRECTION ( 'NONE',  ( -1.000000000000000000, 0.000000000000000000, 0.000000000000000000 ) ) ;
#16228=DIRECTION ( 'NONE',  ( 0.000000000000000000, 0.000000000000000000, -1.000000000000000000 ) ) ;
#16230=CARTESIAN_POINT ( 'NONE',  ( 10.00000000000000000, -20.41355805489602204, -19.44239304137396118 ) ) ;
#16238=CARTESIAN_POINT ( 'NONE',  ( 0.000000000000000000, 20.32630374611208879, -16.60877409751146416 ) ) ;
#16240=CARTESIAN_POINT ( 'NONE',  ( 10.00000000000000000, -32.46095361140696411, 5.940243314904091854 ) ) ;
#16245=LINE ( 'NONE', #2055, #1740 ) ;
#16247=CARTESIAN_POINT ( 'NONE',  ( 10.00000000000000000, 20.41355805489643060, -19.44239304137353841 ) ) ;
#16249=FACE_OUTER_BOUND ( 'NONE', #2366, .T. ) ;
#16250=VERTEX_POINT ( 'NONE', #13422 ) ;
#16253=DIRECTION ( 'NONE',  ( -1.000000000000000000, -0.000000000000000000, -0.000000000000000000 ) ) ;
#16256=VERTEX_POINT ( 'NONE', #16373 ) ;
#16259=ORIENTED_EDGE ( 'NONE', *, *, #9100, .F. ) ;
#16260=CARTESIAN_POINT ( 'NONE',  ( 10.00000000000000000, 0.000000000000000000, 0.000000000000000000 ) ) ;
#16266=DIRECTION ( 'NONE',  ( 0.000000000000000000, 0.000000000000000000, 1.000000000000000000 ) ) ;
#16274=VERTEX_POINT ( 'NONE', #4466 ) ;
#16280=CARTESIAN_POINT ( 'NONE',  ( 10.00000000000000000, -1.489278925039337453, -26.20671763660629949 ) ) ;
#16283=ADVANCED_FACE ( 'NONE', ( #4737 ), #10450, .T. ) ;
#16286=DIRECTION ( 'NONE',  ( -1.000000000000000000, 0.000000000000000000, 0.000000000000000000 ) ) ;
#16293=DIRECTION ( 'NONE',  ( 0.000000000000000000, 0.000000000000000000, 1.000000000000000000 ) ) ;
#16298=ORIENTED_EDGE ( 'NONE', *, *, #5402, .T. ) ;
#16299=DIRECTION ( 'NONE',  ( 0.000000000000000000, 0.000000000000000000, -1.000000000000000000 ) ) ;
#16306=AXIS2_PLACEMENT_3D ( 'NONE', #12521, #12427, #10986 ) ;
#16320=CIRCLE ( 'NONE', #8113, 26.24900000002624978 ) ;
#16321=CARTESIAN_POINT ( 'NONE',  ( 10.00000000000000000, -32.46095361140688595, -5.940243314904558147 ) ) ;
#16323=LINE ( 'NONE', #516, #6566 ) ;
#16325=DIRECTION ( 'NONE',  ( -1.000000000000000000, 0.000000000000000000, 0.000000000000000000 ) ) ;
#16333=EDGE_CURVE ( 'NONE', #6635, #7978, #7684, .T. ) ;
#16340=EDGE_CURVE ( 'NONE', #4319, #17432, #12001, .T. ) ;
#16344=ORIENTED_EDGE ( 'NONE', *, *, #5107, .T. ) ;
#16345=DIRECTION ( 'NONE',  ( 0.000000000000000000, 0.000000000000000000, -1.000000000000000000 ) ) ;
#16349=FACE_OUTER_BOUND ( 'NONE', #6487, .T. ) ;
#16350=EDGE_LOOP ( 'NONE', ( #10458, #11722, #3775, #16298 ) ) ;
#16365=AXIS2_PLACEMENT_3D ( 'NONE', #6418, #14996, #8895 ) ;
#16369=ORIENTED_EDGE ( 'NONE', *, *, #10636, .T. ) ;
#16372=DIRECTION ( 'NONE',  ( 1.000000000000000000, 0.000000000000000000, -0.000000000000000000 ) ) ;
#16373=CARTESIAN_POINT ( 'NONE',  ( 0.000000000000000000, -29.03656532225551601, -15.68049343256028294 ) ) ;
#16392=VECTOR ( 'NONE', #1618, 1000.000000000000000 ) ;
#16396=AXIS2_PLACEMENT_3D ( 'NONE', #4203, #12869, #18668 ) ;
#16398=CARTESIAN_POINT ( 'NONE',  ( 10.00000000000000000, 0.000000000000000000, 0.000000000000000000 ) ) ;
#16420=CARTESIAN_POINT ( 'NONE',  ( 10.00000000000000000, -20.32630374611172641, -16.60877409751190470 ) ) ;
#16422=ORIENTED_EDGE ( 'NONE', *, *, #7387, .T. ) ;
#16425=DIRECTION ( 'NONE',  ( 0.000000000000000000, 1.000000000000000000, 0.000000000000000000 ) ) ;
#16428=VERTEX_POINT ( 'NONE', #6457 ) ;
#16429=ORIENTED_EDGE ( 'NONE', *, *, #14347, .T. ) ;
#16436=DIRECTION ( 'NONE',  ( -1.000000000000000000, -0.000000000000000000, -0.000000000000000000 ) ) ;
#16438=LINE ( 'NONE', #3389, #6310 ) ;
#16440=EDGE_CURVE ( 'NONE', #16450, #5831, #13539, .T. ) ;
#16450=VERTEX_POINT ( 'NONE', #3789 ) ;
#16460=EDGE_CURVE ( 'NONE', #7904, #18365, #9254, .T. ) ;
#16464=CARTESIAN_POINT ( 'NONE',  ( 0.000000000000000000, 14.19907017806900207, -22.07705612348824076 ) ) ;
#16495=VERTEX_POINT ( 'NONE', #9408 ) ;
#16499=CARTESIAN_POINT ( 'NONE',  ( 50.00005079999999680, 0.000000000000000000, 0.000000000000000000 ) ) ;
#16504=DIRECTION ( 'NONE',  ( 0.000000000000000000, 0.000000000000000000, 1.000000000000000000 ) ) ;
#16506=CARTESIAN_POINT ( 'NONE',  ( 5.000000000000000000, 32.70783759231086663, -4.381479206523104963 ) ) ;
#16510=EDGE_CURVE ( 'NONE', #24, #262, #1663, .T. ) ;
#16512=DIRECTION ( 'NONE',  ( -1.000000000000000000, -0.000000000000000000, 0.000000000000000000 ) ) ;
#16513=DIRECTION ( 'NONE',  ( -1.000000000000000000, -0.000000000000000000, 0.000000000000000000 ) ) ;
#16517=VERTEX_POINT ( 'NONE', #10329 ) ;
#16518=AXIS2_PLACEMENT_3D ( 'NONE', #5905, #1895, #9038 ) ;
#16525=VECTOR ( 'NONE', #17570, 1000.000000000000000 ) ;
#16529=ORIENTED_EDGE ( 'NONE', *, *, #14547, .T. ) ;
#16549=DIRECTION ( 'NONE',  ( 1.000000000000000000, 0.000000000000000000, 0.000000000000000000 ) ) ;
#16562=EDGE_CURVE ( 'NONE', #14980, #5515, #3437, .T. ) ;
#16568=EDGE_LOOP ( 'NONE', ( #15440, #11798, #12274, #18497 ) ) ;
#16572=EDGE_CURVE ( 'NONE', #16274, #15320, #14072, .T. ) ;
#16574=DIRECTION ( 'NONE',  ( -1.000000000000000000, 0.000000000000000000, 0.000000000000000000 ) ) ;
#16575=AXIS2_PLACEMENT_3D ( 'NONE', #2912, #8720, #344 ) ;
#16585=CIRCLE ( 'NONE', #6552, 12.00000000001200462 ) ;
#16587=VERTEX_POINT ( 'NONE', #11217 ) ;
#16591=CARTESIAN_POINT ( 'NONE',  ( 10.00000000000000000, 0.000000000000000000, 26.24900000002624978 ) ) ;
#16596=LINE ( 'NONE', #6316, #11337 ) ;
#16607=AXIS2_PLACEMENT_3D ( 'NONE', #18416, #5375, #15570 ) ;
#16609=CIRCLE ( 'NONE', #3802, 12.00000000001200640 ) ;
#16610=DIRECTION ( 'NONE',  ( -1.000000000000000000, -0.000000000000000000, -0.000000000000000000 ) ) ;
#16619=CIRCLE ( 'NONE', #10828, 12.00000000001200640 ) ;
#16624=ORIENTED_EDGE ( 'NONE', *, *, #6437, .T. ) ;
#16633=CARTESIAN_POINT ( 'NONE',  ( 0.000000000000000000, -20.41355805489602204, -19.44239304137396118 ) ) ;
#16641=CARTESIAN_POINT ( 'NONE',  ( 10.00000000000000000, 0.000000000000000000, 0.000000000000000000 ) ) ;
#16643=DIRECTION ( 'NONE',  ( 0.000000000000000000, 0.000000000000000000, 1.000000000000000000 ) ) ;
#16661=ORIENTED_EDGE ( 'NONE', *, *, #11665, .T. ) ;
#16664=CIRCLE ( 'NONE', #7528, 12.00000000001200462 ) ;
#16666=AXIS2_PLACEMENT_3D ( 'NONE', #7002, #14242, #10135 ) ;
#16670=ORIENTED_EDGE ( 'NONE', *, *, #13897, .F. ) ;
#16678=FACE_OUTER_BOUND ( 'NONE', #8564, .T. ) ;
#16682=CIRCLE ( 'NONE', #2693, 33.00000000003299760 ) ;
#16693=VERTEX_POINT ( 'NONE', #16420 ) ;
#16699=CARTESIAN_POINT ( 'NONE',  ( 10.00000000000000000, -19.44239304137360946, -20.41355805489636310 ) ) ;
#16702=EDGE_CURVE ( 'NONE', #17432, #13289, #16596, .T. ) ;
#16707=DIRECTION ( 'NONE',  ( 0.000000000000000000, -0.9510565162951500895, -0.3090169943749581649 ) ) ;
#16711=ORIENTED_EDGE ( 'NONE', *, *, #14641, .F. ) ;
#16713=EDGE_CURVE ( 'NONE', #7504, #944, #14383, .T. ) ;
#16718=ADVANCED_FACE ( 'NONE', ( #4971 ), #12123, .T. ) ;
#16721=CARTESIAN_POINT ( 'NONE',  ( 0.000000000000000000, -12.18267823974769293, 25.42247726998010648 ) ) ;
#16727=CARTESIAN_POINT ( 'NONE',  ( 10.00000000000000000, 29.03656532225586062, -15.68049343255964523 ) ) ;
#16731=LINE ( 'NONE', #18049, #18188 ) ;
#16735=CIRCLE ( 'NONE', #8515, 12.00000000001200462 ) ;
#16741=DIRECTION ( 'NONE',  ( -1.000000000000000000, -0.000000000000000000, -0.000000000000000000 ) ) ;
#16743=DIRECTION ( 'NONE',  ( 0.000000000000000000, -0.5877852522924624790, -0.8090169943749551118 ) ) ;
#16750=CARTESIAN_POINT ( 'NONE',  ( 10.00000000000000000, -19.44239304137360946, -20.41355805489636310 ) ) ;
#16759=CARTESIAN_POINT ( 'NONE',  ( 10.00000000000000000, 19.44239304137375868, 20.41355805489622455 ) ) ;
#16761=FACE_OUTER_BOUND ( 'NONE', #14343, .T. ) ;
#16762=DIRECTION ( 'NONE',  ( -1.000000000000000000, 0.000000000000000000, -0.000000000000000000 ) ) ;
#16766=EDGE_CURVE ( 'NONE', #17515, #18364, #15288, .T. ) ;
#16774=AXIS2_PLACEMENT_3D ( 'NONE', #10432, #73, #16345 ) ;
#16782=ORIENTED_EDGE ( 'NONE', *, *, #15356, .T. ) ;
#16793=LINE ( 'NONE', #2304, #10995 ) ;
#16796=CARTESIAN_POINT ( 'NONE',  ( 10.00000000000000000, 0.000000000000000000, 0.000000000000000000 ) ) ;
#16805=DIRECTION ( 'NONE',  ( 0.000000000000000000, 1.000000000000000000, 3.491481338843133355E-15 ) ) ;
#16813=DIRECTION ( 'NONE',  ( -1.000000000000000000, 0.000000000000000000, 0.000000000000000000 ) ) ;
#16814=ORIENTED_EDGE ( 'NONE', *, *, #12564, .T. ) ;
#16818=ORIENTED_EDGE ( 'NONE', *, *, #9457, .T. ) ;
#16820=ORIENTED_EDGE ( 'NONE', *, *, #12039, .T. ) ;
#16822=EDGE_CURVE ( 'NONE', #10550, #6419, #102, .T. ) ;
#16826=ORIENTED_EDGE ( 'NONE', *, *, #16713, .F. ) ;
#16843=ORIENTED_EDGE ( 'NONE', *, *, #10405, .T. ) ;
#16844=DIRECTION ( 'NONE',  ( 1.000000000000000000, 0.000000000000000000, 0.000000000000000000 ) ) ;
#16852=ORIENTED_EDGE ( 'NONE', *, *, #13871, .T. ) ;
#16861=DIRECTION ( 'NONE',  ( 1.000000000000000000, 0.000000000000000000, 0.000000000000000000 ) ) ;
#16874=EDGE_CURVE ( 'NONE', #11197, #1295, #16793, .T. ) ;
#16878=CARTESIAN_POINT ( 'NONE',  ( 50.00005079999999680, 6.123233995736766282E-16, -5.000000000000000000 ) ) ;
#16879=DIRECTION ( 'NONE',  ( 0.000000000000000000, 0.000000000000000000, 1.000000000000000000 ) ) ;
#16881=CARTESIAN_POINT ( 'NONE',  ( 0.000000000000000000, 6.123233995736766282E-16, -5.000000000000000000 ) ) ;
#16884=DIRECTION ( 'NONE',  ( 0.000000000000000000, 0.8090169943749485615, -0.5877852522924714718 ) ) ;
#16889=CARTESIAN_POINT ( 'NONE',  ( -10.00000000000000000, 0.000000000000000000, 0.000000000000000000 ) ) ;
#16906=VECTOR ( 'NONE', #4346, 1000.000000000000000 ) ;
#16912=EDGE_CURVE ( 'NONE', #18379, #24, #10390, .T. ) ;
#16914=CARTESIAN_POINT ( 'NONE',  ( 5.000000000000000000, 14.27431201565524788, 29.75305054077477607 ) ) ;
#16916=DIRECTION ( 'NONE',  ( 0.000000000000000000, 0.3090169943749410120, 0.9510565162951556406 ) ) ;
#16918=ORIENTED_EDGE ( 'NONE', *, *, #10036, .F. ) ;
#16923=AXIS2_PLACEMENT_3D ( 'NONE', #914, #16610, #2224 ) ;
#16925=AXIS2_PLACEMENT_3D ( 'NONE', #11729, #17719, #207 ) ;
#16938=CARTESIAN_POINT ( 'NONE',  ( 0.000000000000000000, 25.38428207620322752, 6.681932690257054830 ) ) ;
#16946=CYLINDRICAL_SURFACE ( 'NONE', #4345, 12.00000000001200462 ) ;
#16958=ORIENTED_EDGE ( 'NONE', *, *, #7499, .F. ) ;
#16962=DIRECTION ( 'NONE',  ( 0.000000000000000000, 0.000000000000000000, -1.000000000000000000 ) ) ;
#16965=LINE ( 'NONE', #14196, #1472 ) ;
#16966=DIRECTION ( 'NONE',  ( -1.000000000000000000, 0.000000000000000000, 0.000000000000000000 ) ) ;
#16967=CIRCLE ( 'NONE', #2058, 33.00000000003299760 ) ;
#16971=CARTESIAN_POINT ( 'NONE',  ( 0.000000000000000000, 29.75305054077472633, 14.27431201565535979 ) ) ;
#16976=AXIS2_PLACEMENT_3D ( 'NONE', #1628, #18789, #3155 ) ;
#16977=EDGE_CURVE ( 'NONE', #9630, #5675, #13446, .T. ) ;
#16989=CARTESIAN_POINT ( 'NONE',  ( 0.000000000000000000, 0.000000000000000000, 0.000000000000000000 ) ) ;
#16991=DIRECTION ( 'NONE',  ( 0.000000000000000000, 0.000000000000000000, 1.000000000000000000 ) ) ;
#16996=ORIENTED_EDGE ( 'NONE', *, *, #4566, .F. ) ;
#17012=DIRECTION ( 'NONE',  ( -1.000000000000000000, 0.000000000000000000, 0.000000000000000000 ) ) ;
#17014=CIRCLE ( 'NONE', #17314, 12.00000000001200817 ) ;
#17015=CARTESIAN_POINT ( 'NONE',  ( 0.000000000000000000, -14.27431201565505425, -29.75305054077487199 ) ) ;
#17023=DIRECTION ( 'NONE',  ( -1.000000000000000000, -0.000000000000000000, -0.000000000000000000 ) ) ;
#17027=CARTESIAN_POINT ( 'NONE',  ( 0.000000000000000000, -25.42247726998023083, 12.18267823974742470 ) ) ;
#17029=EDGE_LOOP ( 'NONE', ( #9312, #4130, #6801, #15234 ) ) ;
#17036=CARTESIAN_POINT ( 'NONE',  ( 0.000000000000000000, 27.72801475327282361, 6.913036516934699449 ) ) ;
#17038=DIRECTION ( 'NONE',  ( -1.000000000000000000, -0.000000000000000000, 0.000000000000000000 ) ) ;
#17041=PRODUCT_DEFINITION_CONTEXT ( 'detailed design', #15708, 'design' ) ;
#17042=CYLINDRICAL_SURFACE ( 'NONE', #9339, 26.24900000002624978 ) ;
#17046=DIRECTION ( 'NONE',  ( -1.000000000000000000, 0.000000000000000000, 0.000000000000000000 ) ) ;
#17047=EDGE_LOOP ( 'NONE', ( #10251, #1866, #18781, #6810 ) ) ;
#17049=CYLINDRICAL_SURFACE ( 'NONE', #14266, 12.00000000001200462 ) ;
#17050=CARTESIAN_POINT ( 'NONE',  ( 10.00000000000000000, -24.79895094899269026, 13.40641754777657013 ) ) ;
#17056=FACE_OUTER_BOUND ( 'NONE', #3044, .T. ) ;
#17069=DIRECTION ( 'NONE',  ( 0.000000000000000000, 0.000000000000000000, 1.000000000000000000 ) ) ;
#17071=CARTESIAN_POINT ( 'NONE',  ( 10.00000000000000000, -29.75305054077482225, 14.27431201565513597 ) ) ;
#17080=VERTEX_POINT ( 'NONE', #10027 ) ;
#17084=CARTESIAN_POINT ( 'NONE',  ( 10.00000000000000000, 0.000000000000000000, 0.000000000000000000 ) ) ;
#17096=ORIENTED_EDGE ( 'NONE', *, *, #7990, .T. ) ;
#17098=CIRCLE ( 'NONE', #965, 26.24900000002625333 ) ;
#17105=CARTESIAN_POINT ( 'NONE',  ( 0.000000000000000000, 0.000000000000000000, 0.000000000000000000 ) ) ;
#17111=CARTESIAN_POINT ( 'NONE',  ( 10.00000000000000000, 0.000000000000000000, 0.000000000000000000 ) ) ;
#17122=ADVANCED_FACE ( 'NONE', ( #14968 ), #13358, .T. ) ;
#17140=DIRECTION ( 'NONE',  ( 0.000000000000000000, 0.000000000000000000, 1.000000000000000000 ) ) ;
#17143=CARTESIAN_POINT ( 'NONE',  ( 0.000000000000000000, 0.000000000000000000, 1.500000000000000000 ) ) ;
#17160=DIRECTION ( 'NONE',  ( -1.000000000000000000, 0.000000000000000000, -0.000000000000000000 ) ) ;
#17163=CARTESIAN_POINT ( 'NONE',  ( 10.00000000000000000, 6.681932690257323060, -25.38428207620315291 ) ) ;
#17194=CARTESIAN_POINT ( 'NONE',  ( 0.000000000000000000, -22.07705612348849655, 14.19907017806860949 ) ) ;
#17197=CARTESIAN_POINT ( 'NONE',  ( 10.00000000000000000, -12.18267823974732522, -25.42247726998028057 ) ) ;
#17200=DIRECTION ( 'NONE',  ( -1.000000000000000000, -0.000000000000000000, -0.000000000000000000 ) ) ;
#17211=DIRECTION ( 'NONE',  ( -1.000000000000000000, 0.000000000000000000, 0.000000000000000000 ) ) ;
#17228=AXIS2_PLACEMENT_3D ( 'NONE', #3281, #7737, #11759 ) ;
#17243=VECTOR ( 'NONE', #6977, 1000.000000000000000 ) ;
#17244=ORIENTED_EDGE ( 'NONE', *, *, #15524, .T. ) ;
#17253=LINE ( 'NONE', #8574, #3961 ) ;
#17256=ORIENTED_EDGE ( 'NONE', *, *, #9100, .T. ) ;
#17258=AXIS2_PLACEMENT_3D ( 'NONE', #2554, #6838, #17140 ) ;
#17263=EDGE_CURVE ( 'NONE', #9630, #6348, #5709, .T. ) ;
#17264=ORIENTED_EDGE ( 'NONE', *, *, #15478, .F. ) ;
#17265=DIRECTION ( 'NONE',  ( -1.000000000000000000, 0.000000000000000000, 0.000000000000000000 ) ) ;
#17291=CIRCLE ( 'NONE', #16666, 33.00000000003299760 ) ;
#17294=CARTESIAN_POINT ( 'NONE',  ( 10.00000000000000000, 19.44239304137403579, -20.41355805489595454 ) ) ;
#17299=ADVANCED_FACE ( 'NONE', ( #16173 ), #3040, .T. ) ;
#17300=DIRECTION ( 'NONE',  ( -1.000000000000000000, 0.000000000000000000, -0.000000000000000000 ) ) ;
#17304=CARTESIAN_POINT ( 'NONE',  ( 0.000000000000000000, 29.75305054077492173, -14.27431201565494767 ) ) ;
#17306=CARTESIAN_POINT ( 'NONE',  ( 0.000000000000000000, 16.60877409751197575, -20.32630374611166957 ) ) ;
#17310=AXIS2_PLACEMENT_3D ( 'NONE', #8950, #17722, #16293 ) ;
#17311=CARTESIAN_POINT ( 'NONE',  ( 0.000000000000000000, -32.46095361140696411, 5.940243314904091854 ) ) ;
#17314=AXIS2_PLACEMENT_3D ( 'NONE', #11286, #8435, #18619 ) ;
#17317=CIRCLE ( 'NONE', #4825, 26.24900000002625333 ) ;
#17320=DIRECTION ( 'NONE',  ( -1.000000000000000000, 0.000000000000000000, -0.000000000000000000 ) ) ;
#17327=CARTESIAN_POINT ( 'NONE',  ( 10.00000000000000000, -32.70783759231083110, -4.381479206523328784 ) ) ;
#17329=CIRCLE ( 'NONE', #12158, 26.24900000002625333 ) ;
#17335=CYLINDRICAL_SURFACE ( 'NONE', #2718, 12.00000000001200462 ) ;
#17340=ORIENTED_EDGE ( 'NONE', *, *, #11844, .F. ) ;
#17346=FACE_OUTER_BOUND ( 'NONE', #13478, .T. ) ;
#17355=AXIS2_PLACEMENT_3D ( 'NONE', #4054, #9853, #15663 ) ;
#17358=VERTEX_POINT ( 'NONE', #178 ) ;
#17360=FACE_OUTER_BOUND ( 'NONE', #1578, .T. ) ;
#17363=( NAMED_UNIT ( * ) PLANE_ANGLE_UNIT ( ) SI_UNIT ( $, .RADIAN. ) );
#17366=CARTESIAN_POINT ( 'NONE',  ( 10.00000000000000000, 26.20671763660628528, 1.489278925039608570 ) ) ;
#17368=DIRECTION ( 'NONE',  ( 0.000000000000000000, 0.000000000000000000, 1.000000000000000000 ) ) ;
#17377=AXIS2_PLACEMENT_3D ( 'NONE', #13071, #11904, #26 ) ;
#17382=DIRECTION ( 'NONE',  ( 0.000000000000000000, -0.5877852522924623679, -0.8090169943749552228 ) ) ;
#17386=CARTESIAN_POINT ( 'NONE',  ( 10.00000000000000000, -27.72801475327278453, 6.913036516934497833 ) ) ;
#17387=DIRECTION ( 'NONE',  ( 0.000000000000000000, 0.000000000000000000, 1.000000000000000000 ) ) ;
#17388=ORIENTED_EDGE ( 'NONE', *, *, #9228, .F. ) ;
#17406=ORIENTED_EDGE ( 'NONE', *, *, #13257, .T. ) ;
#17410=VERTEX_POINT ( 'NONE', #5444 ) ;
#17417=CIRCLE ( 'NONE', #381, 12.00000000001200462 ) ;
#17418=EDGE_CURVE ( 'NONE', #9007, #3135, #2478, .T. ) ;
#17428=LINE ( 'NONE', #4379, #8190 ) ;
#17432=VERTEX_POINT ( 'NONE', #17071 ) ;
#17434=CARTESIAN_POINT ( 'NONE',  ( 0.000000000000000000, -25.38428207620327370, 6.681932690256871865 ) ) ;
#17437=DIRECTION ( 'NONE',  ( -1.000000000000000000, -0.000000000000000000, 0.000000000000000000 ) ) ;
#17438=DIRECTION ( 'NONE',  ( 0.000000000000000000, 0.000000000000000000, -1.000000000000000000 ) ) ;
#17453=VERTEX_POINT ( 'NONE', #18377 ) ;
#17456=FACE_BOUND ( 'NONE', #10365, .T. ) ;
#17470=CARTESIAN_POINT ( 'NONE',  ( 10.00000000000000000, -32.70783759231088794, 4.381479206522872261 ) ) ;
#17484=CARTESIAN_POINT ( 'NONE',  ( 10.00000000000000000, 27.72801475327282361, -5.086963483077305170 ) ) ;
#17491=ORIENTED_EDGE ( 'NONE', *, *, #15065, .T. ) ;
#17493=EDGE_CURVE ( 'NONE', #6780, #3169, #17708, .T. ) ;
#17496=ORIENTED_EDGE ( 'NONE', *, *, #15230, .F. ) ;
#17498=FACE_OUTER_BOUND ( 'NONE', #8402, .T. ) ;
#17499=EDGE_CURVE ( 'NONE', #4272, #684, #18481, .T. ) ;
#17500=ORIENTED_EDGE ( 'NONE', *, *, #18405, .T. ) ;
#17504=CIRCLE ( 'NONE', #3527, 12.00000000001200107 ) ;
#17514=CARTESIAN_POINT ( 'NONE',  ( 10.00000000000000000, -25.38428207620327370, 6.681932690256871865 ) ) ;
#17515=VERTEX_POINT ( 'NONE', #18763 ) ;
#17519=CIRCLE ( 'NONE', #190, 26.24900000002624978 ) ;
#17532=AXIS2_PLACEMENT_3D ( 'NONE', #8251, #15489, #2334 ) ;
#17535=CARTESIAN_POINT ( 'NONE',  ( 10.00000000000000000, -25.38428207620317778, -6.681932690257235130 ) ) ;
#17543=CARTESIAN_POINT ( 'NONE',  ( 10.00000000000000000, 3.730438010304726770, -27.94286728106388296 ) ) ;
#17549=PLANE ( 'NONE',  #15772 ) ;
#17551=AXIS2_PLACEMENT_3D ( 'NONE', #203, #14761, #16643 ) ;
#17569=CARTESIAN_POINT ( 'NONE',  ( 10.00000000000000000, 27.72801475327274900, 5.086963483077687975 ) ) ;
#17570=DIRECTION ( 'NONE',  ( -1.000000000000000000, 0.000000000000000000, 0.000000000000000000 ) ) ;
#17571=DIRECTION ( 'NONE',  ( -1.000000000000000000, 0.000000000000000000, 0.000000000000000000 ) ) ;
#17578=AXIS2_PLACEMENT_3D ( 'NONE', #7360, #12812, #18706 ) ;
#17581=CARTESIAN_POINT ( 'NONE',  ( 5.000000000000000000, -23.88582760061497368, 22.76987570971518338 ) ) ;
#17584=VERTEX_POINT ( 'NONE', #285 ) ;
#17589=DIRECTION ( 'NONE',  ( -1.000000000000000000, 0.000000000000000000, -0.000000000000000000 ) ) ;
#17590=VERTEX_POINT ( 'NONE', #10372 ) ;
#17605=ORIENTED_EDGE ( 'NONE', *, *, #2482, .F. ) ;
#17607=VERTEX_POINT ( 'NONE', #11807 ) ;
#17620=CARTESIAN_POINT ( 'NONE',  ( 10.00000000000000000, 25.42247726998032320, -12.18267823974723640 ) ) ;
#17626=AXIS2_PLACEMENT_3D ( 'NONE', #3235, #1615, #3341 ) ;
#17627=AXIS2_PLACEMENT_3D ( 'NONE', #10967, #17935, #16884 ) ;
#17635=CARTESIAN_POINT ( 'NONE',  ( 10.00000000000000000, 25.38428207620331634, -6.681932690256706664 ) ) ;
#17638=CIRCLE ( 'NONE', #1223, 33.00000000003299760 ) ;
#17640=DIRECTION ( 'NONE',  ( -1.000000000000000000, 0.000000000000000000, -0.000000000000000000 ) ) ;
#17655=DIRECTION ( 'NONE',  ( 0.000000000000000000, 0.000000000000000000, 1.000000000000000000 ) ) ;
#17656=CARTESIAN_POINT ( 'NONE',  ( 10.00000000000000000, 0.000000000000000000, 0.000000000000000000 ) ) ;
#17665=CYLINDRICAL_SURFACE ( 'NONE', #14409, 26.24900000002624978 ) ;
#17666=DIRECTION ( 'NONE',  ( -1.000000000000000000, -0.000000000000000000, -0.000000000000000000 ) ) ;
#17668=ORIENTED_EDGE ( 'NONE', *, *, #10170, .T. ) ;
#17690=FACE_OUTER_BOUND ( 'NONE', #2577, .T. ) ;
#17696=ORIENTED_EDGE ( 'NONE', *, *, #3498, .T. ) ;
#17708=CIRCLE ( 'NONE', #14369, 26.24900000002624978 ) ;
#17709=EDGE_LOOP ( 'NONE', ( #2462, #7244, #11436, #16958 ) ) ;
#17711=DIRECTION ( 'NONE',  ( -1.000000000000000000, 0.000000000000000000, 0.000000000000000000 ) ) ;
#17716=ORIENTED_EDGE ( 'NONE', *, *, #1273, .F. ) ;
#17719=DIRECTION ( 'NONE',  ( -1.000000000000000000, -0.000000000000000000, -0.000000000000000000 ) ) ;
#17722=DIRECTION ( 'NONE',  ( -1.000000000000000000, -0.000000000000000000, -0.000000000000000000 ) ) ;
#17725=EDGE_LOOP ( 'NONE', ( #1915, #9690, #17919, #18404 ) ) ;
#17732=AXIS2_PLACEMENT_3D ( 'NONE', #2836, #8637, #13032 ) ;
#17739=DIRECTION ( 'NONE',  ( -1.000000000000000000, -0.000000000000000000, 0.000000000000000000 ) ) ;
#17753=ORIENTED_EDGE ( 'NONE', *, *, #11723, .F. ) ;
#17754=EDGE_CURVE ( 'NONE', #18379, #5754, #13710, .T. ) ;
#17760=DIRECTION ( 'NONE',  ( 1.000000000000000000, 0.000000000000000000, 0.000000000000000000 ) ) ;
#17766=CARTESIAN_POINT ( 'NONE',  ( 0.000000000000000000, -14.19907017806883864, 22.07705612348834734 ) ) ;
#17774=( NAMED_UNIT ( * ) SI_UNIT ( $, .STERADIAN. ) SOLID_ANGLE_UNIT ( ) );
#17776=CARTESIAN_POINT ( 'NONE',  ( 0.000000000000000000, -32.46095361140688595, -5.940243314904558147 ) ) ;
#17778=DIRECTION ( 'NONE',  ( -1.000000000000000000, -0.000000000000000000, -0.000000000000000000 ) ) ;
#17781=ORIENTED_EDGE ( 'NONE', *, *, #18266, .F. ) ;
#17803=ORIENTED_EDGE ( 'NONE', *, *, #15700, .F. ) ;
#17807=DIRECTION ( 'NONE',  ( 0.000000000000000000, 0.000000000000000000, 1.000000000000000000 ) ) ;
#17817=ORIENTED_EDGE ( 'NONE', *, *, #17499, .T. ) ;
#17820=EDGE_CURVE ( 'NONE', #5675, #3305, #13474, .T. ) ;
#17821=VERTEX_POINT ( 'NONE', #14079 ) ;
#17822=CIRCLE ( 'NONE', #6868, 12.00000000001200817 ) ;
#17830=EDGE_CURVE ( 'NONE', #10460, #7525, #17417, .T. ) ;
#17850=CARTESIAN_POINT ( 'NONE',  ( 0.000000000000000000, 0.000000000000000000, 0.000000000000000000 ) ) ;
#17861=ADVANCED_FACE ( 'NONE', ( #9884 ), #16946, .T. ) ;
#17862=DIRECTION ( 'NONE',  ( -1.000000000000000000, 0.000000000000000000, 0.000000000000000000 ) ) ;
#17867=AXIS2_PLACEMENT_3D ( 'NONE', #5351, #6875, #7227 ) ;
#17871=AXIS2_PLACEMENT_3D ( 'NONE', #12599, #3749, #9548 ) ;
#17884=VECTOR ( 'NONE', #5443, 1000.000000000000000 ) ;
#17891=DIRECTION ( 'NONE',  ( -1.000000000000000000, 0.000000000000000000, 0.000000000000000000 ) ) ;
#17896=CIRCLE ( 'NONE', #2994, 33.00000000003299760 ) ;
#17899=CARTESIAN_POINT ( 'NONE',  ( 0.000000000000000000, -24.46385708179990459, 9.514709542736804693 ) ) ;
#17900=AXIS2_PLACEMENT_3D ( 'NONE', #2962, #6182, #377 ) ;
#17912=ORIENTED_EDGE ( 'NONE', *, *, #12267, .T. ) ;
#17918=DIRECTION ( 'NONE',  ( 0.000000000000000000, -0.8090169943749531134, 0.5877852522924653655 ) ) ;
#17919=ORIENTED_EDGE ( 'NONE', *, *, #14169, .T. ) ;
#17921=CARTESIAN_POINT ( 'NONE',  ( 0.000000000000000000, 27.94286728106393269, 15.73043801031642808 ) ) ;
#17930=DIRECTION ( 'NONE',  ( 0.000000000000000000, 0.000000000000000000, 1.000000000000000000 ) ) ;
#17931=DIRECTION ( 'NONE',  ( 0.000000000000000000, 0.000000000000000000, 1.000000000000000000 ) ) ;
#17933=DIRECTION ( 'NONE',  ( -1.000000000000000000, 0.000000000000000000, -0.000000000000000000 ) ) ;
#17935=DIRECTION ( 'NONE',  ( -1.000000000000000000, 0.000000000000000000, -0.000000000000000000 ) ) ;
#17937=DIRECTION ( 'NONE',  ( -1.000000000000000000, -0.000000000000000000, -0.000000000000000000 ) ) ;
#17951=ORIENTED_EDGE ( 'NONE', *, *, #8812, .F. ) ;
#17968=ORIENTED_EDGE ( 'NONE', *, *, #17263, .F. ) ;
#17979=EDGE_LOOP ( 'NONE', ( #13456, #12833, #6064, #13080 ) ) ;
#17988=CARTESIAN_POINT ( 'NONE',  ( 0.000000000000000000, 25.42247726998014912, 12.18267823974760411 ) ) ;
#17997=ORIENTED_EDGE ( 'NONE', *, *, #744, .F. ) ;
#18008=CARTESIAN_POINT ( 'NONE',  ( 10.00000000000000000, -27.94286728106395756, 3.730438010304225394 ) ) ;
#18015=AXIS2_PLACEMENT_3D ( 'NONE', #9167, #17937, #7645 ) ;
#18016=ORIENTED_EDGE ( 'NONE', *, *, #6057, .F. ) ;
#18020=CARTESIAN_POINT ( 'NONE',  ( 0.000000000000000000, 27.94286728106393269, 3.730438010304423013 ) ) ;
#18023=DIRECTION ( 'NONE',  ( 0.000000000000000000, 0.000000000000000000, 1.000000000000000000 ) ) ;
#18024=DIRECTION ( 'NONE',  ( 0.000000000000000000, 0.5877852522924741363, -0.8090169943749466741 ) ) ;
#18028=ORIENTED_EDGE ( 'NONE', *, *, #9457, .F. ) ;
#18029=EDGE_CURVE ( 'NONE', #18365, #17515, #6475, .T. ) ;
#18040=VERTEX_POINT ( 'NONE', #5793 ) ;
#18046=ORIENTED_EDGE ( 'NONE', *, *, #1897, .F. ) ;
#18049=CARTESIAN_POINT ( 'NONE',  ( 5.000000000000000000, -5.940243314904445349, 32.46095361140691438 ) ) ;
#18053=EDGE_LOOP ( 'NONE', ( #9674, #12919, #234, #5539 ) ) ;
#18054=ORIENTED_EDGE ( 'NONE', *, *, #9341, .F. ) ;
#18058=ORIENTED_EDGE ( 'NONE', *, *, #14289, .T. ) ;
#18064=VERTEX_POINT ( 'NONE', #13126 ) ;
#18080=EDGE_CURVE ( 'NONE', #6022, #890, #11034, .T. ) ;
#18100=DIRECTION ( 'NONE',  ( -1.000000000000000000, 0.000000000000000000, -0.000000000000000000 ) ) ;
#18120=FACE_OUTER_BOUND ( 'NONE', #2681, .T. ) ;
#18123=DIRECTION ( 'NONE',  ( 0.000000000000000000, 0.000000000000000000, 1.000000000000000000 ) ) ;
#18125=ORIENTED_EDGE ( 'NONE', *, *, #3646, .T. ) ;
#18127=VECTOR ( 'NONE', #1613, 1000.000000000000000 ) ;
#18137=DIRECTION ( 'NONE',  ( 0.000000000000000000, 0.5877852522924684742, 0.8090169943749506709 ) ) ;
#18141=EDGE_LOOP ( 'NONE', ( #2792, #11109, #1036, #10743 ) ) ;
#18144=CARTESIAN_POINT ( 'NONE',  ( 0.000000000000000000, 0.000000000000000000, 0.000000000000000000 ) ) ;
#18147=CARTESIAN_POINT ( 'NONE',  ( 10.00000000000000000, 16.60877409751168443, 20.32630374611190405 ) ) ;
#18164=CIRCLE ( 'NONE', #9040, 33.00000000003299760 ) ;
#18169=DIRECTION ( 'NONE',  ( -1.000000000000000000, 0.000000000000000000, 0.000000000000000000 ) ) ;
#18170=DIRECTION ( 'NONE',  ( 0.000000000000000000, 0.000000000000000000, 1.000000000000000000 ) ) ;
#18178=FACE_OUTER_BOUND ( 'NONE', #17029, .T. ) ;
#18186=AXIS2_PLACEMENT_3D ( 'NONE', #5168, #9642, #9541 ) ;
#18188=VECTOR ( 'NONE', #9478, 1000.000000000000000 ) ;
#18194=AXIS2_PLACEMENT_3D ( 'NONE', #5336, #8005, #11144 ) ;
#18204=EDGE_LOOP ( 'NONE', ( #6154, #12924, #13647, #18463 ) ) ;
#18207=AXIS2_PLACEMENT_3D ( 'NONE', #3838, #9648, #12596 ) ;
#18222=CARTESIAN_POINT ( 'NONE',  ( 0.000000000000000000, 0.000000000000000000, 0.000000000000000000 ) ) ;
#18223=ORIENTED_EDGE ( 'NONE', *, *, #13439, .F. ) ;
#18231=ORIENTED_EDGE ( 'NONE', *, *, #14715, .F. ) ;
#18236=EDGE_CURVE ( 'NONE', #18040, #3486, #13780, .T. ) ;
#18239=DIRECTION ( 'NONE',  ( -1.000000000000000000, 0.000000000000000000, -0.000000000000000000 ) ) ;
#18248=DIRECTION ( 'NONE',  ( -1.000000000000000000, 0.000000000000000000, 0.000000000000000000 ) ) ;
#18261=CYLINDRICAL_SURFACE ( 'NONE', #8835, 12.00000000001200284 ) ;
#18266=EDGE_CURVE ( 'NONE', #3895, #205, #9484, .T. ) ;
#18268=DIRECTION ( 'NONE',  ( 0.000000000000000000, 8.881784197001252323E-16, 1.000000000000000000 ) ) ;
#18270=LINE ( 'NONE', #5216, #12114 ) ;
#18271=DIRECTION ( 'NONE',  ( -1.000000000000000000, 0.000000000000000000, -0.000000000000000000 ) ) ;
#18284=CARTESIAN_POINT ( 'NONE',  ( 5.000000000000000000, -29.03656532225574338, 15.68049343255986017 ) ) ;
#18297=EDGE_CURVE ( 'NONE', #17607, #14062, #3686, .T. ) ;
#18300=AXIS2_PLACEMENT_3D ( 'NONE', #4038, #6501, #16707 ) ;
#18316=ORIENTED_EDGE ( 'NONE', *, *, #14370, .F. ) ;
#18317=EDGE_LOOP ( 'NONE', ( #16814, #8725, #11727, #15117 ) ) ;
#18323=ADVANCED_FACE ( 'NONE', ( #2902 ), #14424, .T. ) ;
#18335=DIRECTION ( 'NONE',  ( -1.000000000000000000, -0.000000000000000000, -0.000000000000000000 ) ) ;
#18338=CARTESIAN_POINT ( 'NONE',  ( 0.000000000000000000, 0.000000000000000000, 0.000000000000000000 ) ) ;
#18343=DIRECTION ( 'NONE',  ( -1.000000000000000000, 0.000000000000000000, 0.000000000000000000 ) ) ;
#18344=ORIENTED_EDGE ( 'NONE', *, *, #8931, .T. ) ;
#18347=VECTOR ( 'NONE', #9420, 1000.000000000000000 ) ;
#18351=DIRECTION ( 'NONE',  ( 0.000000000000000000, 0.000000000000000000, 1.000000000000000000 ) ) ;
#18353=DIRECTION ( 'NONE',  ( 0.000000000000000000, 0.000000000000000000, -1.000000000000000000 ) ) ;
#18354=DIRECTION ( 'NONE',  ( 0.000000000000000000, 0.8090169943749445647, 0.5877852522924770229 ) ) ;
#18364=VERTEX_POINT ( 'NONE', #13189 ) ;
#18365=VERTEX_POINT ( 'NONE', #5579 ) ;
#18369=ORIENTED_EDGE ( 'NONE', *, *, #5486, .F. ) ;
#18377=CARTESIAN_POINT ( 'NONE',  ( 0.000000000000000000, -14.19907017806852245, -22.07705612348854984 ) ) ;
#18379=VERTEX_POINT ( 'NONE', #1651 ) ;
#18388=CARTESIAN_POINT ( 'NONE',  ( 10.00000000000000000, -12.18267823974732522, -25.42247726998028057 ) ) ;
#18389=CARTESIAN_POINT ( 'NONE',  ( 5.000000000000000000, 5.940243314904213534, 32.46095361140695701 ) ) ;
#18404=ORIENTED_EDGE ( 'NONE', *, *, #1151, .T. ) ;
#18405=EDGE_CURVE ( 'NONE', #38, #1366, #11760, .T. ) ;
#18416=CARTESIAN_POINT ( 'NONE',  ( 0.000000000000000000, 0.000000000000000000, 0.000000000000000000 ) ) ;
#18426=ORIENTED_EDGE ( 'NONE', *, *, #5862, .T. ) ;
#18431=ORIENTED_EDGE ( 'NONE', *, *, #16822, .T. ) ;
#18434=EDGE_CURVE ( 'NONE', #15870, #17590, #2536, .T. ) ;
#18454=CIRCLE ( 'NONE', #13883, 12.00000000001200462 ) ;
#18463=ORIENTED_EDGE ( 'NONE', *, *, #3767, .T. ) ;
#18465=DIRECTION ( 'NONE',  ( -1.000000000000000000, 0.000000000000000000, -0.000000000000000000 ) ) ;
#18472=VECTOR ( 'NONE', #8816, 1000.000000000000000 ) ;
#18473=AXIS2_PLACEMENT_3D ( 'NONE', #5068, #12214, #18023 ) ;
#18481=LINE ( 'NONE', #11245, #6147 ) ;
#18490=CIRCLE ( 'NONE', #16976, 33.00000000003299760 ) ;
#18494=ADVANCED_FACE ( 'NONE', ( #12026 ), #17665, .T. ) ;
#18497=ORIENTED_EDGE ( 'NONE', *, *, #12961, .F. ) ;
#18501=CIRCLE ( 'NONE', #10292, 12.00000000001200462 ) ;
#18523=AXIS2_PLACEMENT_3D ( 'NONE', #4744, #9030, #14851 ) ;
#18532=CARTESIAN_POINT ( 'NONE',  ( 10.00000000000000000, 0.000000000000000000, 0.000000000000000000 ) ) ;
#18537=ORIENTED_EDGE ( 'NONE', *, *, #6083, .T. ) ;
#18544=CIRCLE ( 'NONE', #13083, 12.00000000001200640 ) ;
#18547=ADVANCED_FACE ( 'NONE', ( #13476 ), #13385, .T. ) ;
#18548=ORIENTED_EDGE ( 'NONE', *, *, #5762, .T. ) ;
#18553=DIRECTION ( 'NONE',  ( 1.000000000000000000, 0.000000000000000000, 0.000000000000000000 ) ) ;
#18555=CARTESIAN_POINT ( 'NONE',  ( 10.00000000000000000, 27.94286728106393269, 3.730438010304423013 ) ) ;
#18558=ORIENTED_EDGE ( 'NONE', *, *, #11905, .T. ) ;
#18563=ORIENTED_EDGE ( 'NONE', *, *, #18236, .T. ) ;
#18564=EDGE_LOOP ( 'NONE', ( #7601, #18796, #2814, #14088 ) ) ;
#18567=ORIENTED_EDGE ( 'NONE', *, *, #11905, .F. ) ;
#18568=DIRECTION ( 'NONE',  ( -1.000000000000000000, 0.000000000000000000, -0.000000000000000000 ) ) ;
#18571=VECTOR ( 'NONE', #15944, 1000.000000000000000 ) ;
#18574=ORIENTED_EDGE ( 'NONE', *, *, #725, .F. ) ;
#18583=ORIENTED_EDGE ( 'NONE', *, *, #14586, .T. ) ;
#18594=ORIENTED_EDGE ( 'NONE', *, *, #14021, .T. ) ;
#18596=DIRECTION ( 'NONE',  ( -1.000000000000000000, 0.000000000000000000, 0.000000000000000000 ) ) ;
#18601=DIRECTION ( 'NONE',  ( 0.000000000000000000, 0.000000000000000000, -1.000000000000000000 ) ) ;
#18604=CARTESIAN_POINT ( 'NONE',  ( 10.00000000000000000, 0.000000000000000000, 0.000000000000000000 ) ) ;
#18613=ADVANCED_FACE ( 'NONE', ( #1847 ), #3378, .T. ) ;
#18614=FACE_OUTER_BOUND ( 'NONE', #16568, .T. ) ;
#18619=DIRECTION ( 'NONE',  ( 0.000000000000000000, 0.000000000000000000, -1.000000000000000000 ) ) ;
#18631=CARTESIAN_POINT ( 'NONE',  ( 10.00000000000000000, 26.20671763660628528, 1.489278925039608570 ) ) ;
#18654=AXIS2_PLACEMENT_3D ( 'NONE', #14392, #17711, #16104 ) ;
#18658=DIRECTION ( 'NONE',  ( -1.000000000000000000, -0.000000000000000000, 0.000000000000000000 ) ) ;
#18659=VERTEX_POINT ( 'NONE', #15651 ) ;
#18662=EDGE_LOOP ( 'NONE', ( #18697, #5734, #4808, #11683 ) ) ;
#18668=DIRECTION ( 'NONE',  ( 0.000000000000000000, 0.000000000000000000, 1.000000000000000000 ) ) ;
#18689=DIRECTION ( 'NONE',  ( 0.000000000000000000, -0.8090169943749402348, -0.5877852522924830181 ) ) ;
#18694=ORIENTED_EDGE ( 'NONE', *, *, #4566, .T. ) ;
#18697=ORIENTED_EDGE ( 'NONE', *, *, #17493, .F. ) ;
#18706=DIRECTION ( 'NONE',  ( 0.000000000000000000, 0.000000000000000000, 1.000000000000000000 ) ) ;
#18712=DIRECTION ( 'NONE',  ( 1.000000000000000000, 0.000000000000000000, 0.000000000000000000 ) ) ;
#18713=CARTESIAN_POINT ( 'NONE',  ( 0.000000000000000000, 0.000000000000000000, 0.000000000000000000 ) ) ;
#18728=DIRECTION ( 'NONE',  ( 0.000000000000000000, 0.5877852522924741363, -0.8090169943749465631 ) ) ;
#18737=ORIENTED_EDGE ( 'NONE', *, *, #13528, .T. ) ;
#18760=CARTESIAN_POINT ( 'NONE',  ( -10.00000000000000000, 0.000000000000000000, 0.000000000000000000 ) ) ;
#18763=CARTESIAN_POINT ( 'NONE',  ( 10.00000000000000000, -22.76987570971544272, 23.88582760061473564 ) ) ;
#18767=FACE_OUTER_BOUND ( 'NONE', #11566, .T. ) ;
#18768=PRODUCT_DEFINITION ( 'UNKNOWN', '', #14449, #17041 ) ;
#18775=AXIS2_PLACEMENT_3D ( 'NONE', #8170, #12832, #15500 ) ;
#18781=ORIENTED_EDGE ( 'NONE', *, *, #8759, .T. ) ;
#18784=DIRECTION ( 'NONE',  ( -1.000000000000000000, 0.000000000000000000, -0.000000000000000000 ) ) ;
#18787=ADVANCED_FACE ( 'NONE', ( #7264, #17456 ), #11363, .F. ) ;
#18789=DIRECTION ( 'NONE',  ( -1.000000000000000000, -0.000000000000000000, -0.000000000000000000 ) ) ;
#18793=VERTEX_POINT ( 'NONE', #11736 ) ;
#18796=ORIENTED_EDGE ( 'NONE', *, *, #15041, .F. ) ;
#18801=ORIENTED_EDGE ( 'NONE', *, *, #13325, .F. ) ;
#18803=AXIS2_PLACEMENT_3D ( 'NONE', #14073, #6741, #852 ) ;
#18806=AXIS2_PLACEMENT_3D ( 'NONE', #11657, #14332, #1200 ) ;
#18808=ORIENTED_EDGE ( 'NONE', *, *, #8215, .T. ) ;
#18884=COLOUR_RGB('Off White',0.89,0.88,0.83);
#18885=FILL_AREA_STYLE_COLOUR('',#18884);
#18886=FILL_AREA_STYLE('',(#18885));
#18887=SURFACE_STYLE_FILL_AREA(#18886);
#18888=SURFACE_SIDE_STYLE('',(#18887));
#18889=SURFACE_STYLE_USAGE(.BOTH.,#18888);
#18890=PRESENTATION_STYLE_ASSIGNMENT((#18889));
ENDSEC;
END-ISO-10303-21;
